ISO-10303-21;
HEADER;
FILE_DESCRIPTION (('STEP AP214'),
    '1' );
FILE_NAME ('Drive Pawl.step',
    '2026-10-06T09:00:30',
    ( '' ),
    ( '' ),
    'SwSTEP 2.0',
    'SolidWorks 2020',
    '' );
FILE_SCHEMA (( 'AUTOMOTIVE_DESIGN' ));
ENDSEC;

DATA;
#19=EDGE_LOOP ( 'NONE', ( #14713, #16983, #4133, #2279 ) ) ;
#23=CARTESIAN_POINT ( 'NONE',  ( -4.903324624900923467, -10.51181958078580259, -35.69001801787404560 ) ) ;
#29=CARTESIAN_POINT ( 'NONE',  ( -6.645959583264284376, -7.251031249533246736, -33.94260493001564782 ) ) ;
#93=( LENGTH_UNIT ( ) NAMED_UNIT ( * ) SI_UNIT ( .MILLI., .METRE. ) );
#97=VERTEX_POINT ( 'NONE', #25833 ) ;
#127=ORIENTED_EDGE ( 'NONE', *, *, #8933, .T. ) ;
#130=EDGE_CURVE ( 'NONE', #97, #8033, #30399, .T. ) ;
#154=CARTESIAN_POINT ( 'NONE',  ( 4.638687372181960811, -19.47448025771016233, -31.31863632548023801 ) ) ;
#157=EDGE_CURVE ( 'NONE', #11921, #14079, #9072, .T. ) ;
#175=CARTESIAN_POINT ( 'NONE',  ( -6.661312627754256255, -8.560122214784900763, -36.64192442629084212 ) ) ;
#180=CARTESIAN_POINT ( 'NONE',  ( -4.861312627776431583, -9.716283825163692711, -32.74022090983473987 ) ) ;
#207=CARTESIAN_POINT ( 'NONE',  ( 7.099269075060530731, -8.189196033044112255, -36.82283721307814517 ) ) ;
#225=B_SPLINE_CURVE_WITH_KNOTS ( 'NONE', 3,
 ( #19407, #7594, #2874, #4928, #17039, #25916 ),
 .UNSPECIFIED., .F., .F.,
 ( 4, 2, 4 ),
 ( 0.000000000000000000, 0.5000000000000000000, 1.000000000000000000 ),
 .UNSPECIFIED. ) ;
#261=( LENGTH_UNIT ( ) NAMED_UNIT ( * ) SI_UNIT ( .MILLI., .METRE. ) );
#266=ORIENTED_EDGE ( 'NONE', *, *, #25247, .T. ) ;
#362=ORIENTED_EDGE ( 'NONE', *, *, #25331, .T. ) ;
#364=FACE_OUTER_BOUND ( 'NONE', #13195, .T. ) ;
#370=CARTESIAN_POINT ( 'NONE',  ( 6.438687372225744276, -8.560122214837054599, -36.64192442626541890 ) ) ;
#404=SURFACE_SIDE_STYLE ('',( #26510 ) ) ;
#487=ORIENTED_EDGE ( 'NONE', *, *, #22114, .T. ) ;
#514=DIRECTION ( 'NONE',  ( -0.7071067811834159667, 0.6355433650310505778, -0.3099752105724544737 ) ) ;
#528=VERTEX_POINT ( 'NONE', #14451 ) ;
#558=ADVANCED_FACE ( 'NONE', ( #1056 ), #28917, .F. ) ;
#562=ORIENTED_EDGE ( 'NONE', *, *, #8040, .F. ) ;
#578=CARTESIAN_POINT ( 'NONE',  ( 1.850829058368554492, -3.930924299794261056, -38.89973510835294235 ) ) ;
#579=EDGE_CURVE ( 'NONE', #21911, #7653, #7180, .T. ) ;
#584=CARTESIAN_POINT ( 'NONE',  ( 2.423529086371690511, -21.74707102514618740, -30.21021974772776986 ) ) ;
#614=CARTESIAN_POINT ( 'NONE',  ( -7.861312627709999390, 2.450513428968473129, -42.01217025057427179 ) ) ;
#661=LINE ( 'NONE', #3612, #30395 ) ;
#710=VECTOR ( 'NONE', #27940, 1000.000000000000000 ) ;
#746=VECTOR ( 'NONE', #11944, 1000.000000000000114 ) ;
#769=VECTOR ( 'NONE', #17966, 1000.000000000000114 ) ;
#786=ORIENTED_EDGE ( 'NONE', *, *, #29103, .T. ) ;
#836=MANIFOLD_SOLID_BREP ( 'PartBody', #31118 ) ;
#854=CARTESIAN_POINT ( 'NONE',  ( -3.916350486798555242, 2.029077553960367819, -38.46881641891648940 ) ) ;
#869=STYLED_ITEM ( 'NONE', ( #24313 ), #836 ) ;
#878=CARTESIAN_POINT ( 'NONE',  ( 6.760007715859398303, 5.672256964398498802, -40.24571374337934770 ) ) ;
#898=CARTESIAN_POINT ( 'NONE',  ( 3.861721477338983632, 0.2146938847481238977, -40.92168819670553148 ) ) ;
#937=ORIENTED_EDGE ( 'NONE', *, *, #11074, .T. ) ;
#1008=CARTESIAN_POINT ( 'NONE',  ( -0.5080847461133405352, 4.304903296726419804, -39.57881079956060688 ) ) ;
#1056=FACE_OUTER_BOUND ( 'NONE', #19, .T. ) ;
#1086=AXIS2_PLACEMENT_3D ( 'NONE', #2652, #28767, #12245 ) ;
#1107=B_SPLINE_CURVE_WITH_KNOTS ( 'NONE', 5,
 ( #18342, #6385, #25594, #4027, #13625, #1670, #26513, #9990, #12040, #12348, #2752, #12182 ),
 .UNSPECIFIED., .F., .F.,
 ( 6, 3, 3, 6 ),
 ( 0.000000000000000000, 2.812352519340000079, 5.624713925070000009, 7.679355244459999952 ),
 .UNSPECIFIED. ) ;
#1142=DIRECTION ( 'NONE',  ( -4.428977494234582379E-12, -0.8987940462991651502, 0.4383711467890810676 ) ) ;
#1144=CARTESIAN_POINT ( 'NONE',  ( 3.827451119382927036, -1.796035916205476424, -39.94098974597989837 ) ) ;
#1148=CARTESIAN_POINT ( 'NONE',  ( -4.861312627776431583, -9.716283825163692711, -32.74022090983473987 ) ) ;
#1187=ADVANCED_FACE ( 'NONE', ( #16518 ), #5026, .F. ) ;
#1308=CARTESIAN_POINT ( 'NONE',  ( 4.638804294843716036, -9.686171446567970023, -32.75490769819511172 ) ) ;
#1312=VERTEX_POINT ( 'NONE', #14166 ) ;
#1330=LINE ( 'NONE', #25245, #14054 ) ;
#1363=ORIENTED_EDGE ( 'NONE', *, *, #22710, .F. ) ;
#1372=CARTESIAN_POINT ( 'NONE',  ( -6.982632971260604116, 4.357143524085962838, -42.94209588230350505 ) ) ;
#1450=CARTESIAN_POINT ( 'NONE',  ( -4.870417428126710746, 6.462009008221302864, -40.63090155203821752 ) ) ;
#1469=CARTESIAN_POINT ( 'NONE',  ( 6.127633414585145211, -7.367024628712027123, -33.88603117893229921 ) ) ;
#1478=CYLINDRICAL_SURFACE ( 'NONE', #29859, 3.000000000000002220 ) ;
#1535=EDGE_CURVE ( 'NONE', #13631, #11921, #27089, .T. ) ;
#1555=ORIENTED_EDGE ( 'NONE', *, *, #14905, .T. ) ;
#1652=AXIS2_PLACEMENT_3D ( 'NONE', #7185, #14277, #21357 ) ;
#1670=CARTESIAN_POINT ( 'NONE',  ( 2.476206779668751246, 3.511840374477381843, -39.19200816759646955 ) ) ;
#1699=CARTESIAN_POINT ( 'NONE',  ( -6.661312627754254478, -7.245008774417666331, -33.94554228739334434 ) ) ;
#1714=VECTOR ( 'NONE', #9605, 1000.000000000000000 ) ;
#1715=PLANE ( 'NONE',  #24649 ) ;
#1728=CARTESIAN_POINT ( 'NONE',  ( 4.978085835933289793, 6.462009008182098668, -40.63090155201910392 ) ) ;
#1746=CARTESIAN_POINT ( 'NONE',  ( 1.850829058368556268, -2.615810859427025736, -36.20335296945545167 ) ) ;
#1757=VERTEX_POINT ( 'NONE', #23702 ) ;
#1809=EDGE_CURVE ( 'NONE', #6144, #22416, #15167, .T. ) ;
#1877=( GEOMETRIC_REPRESENTATION_CONTEXT ( 3 ) GLOBAL_UNCERTAINTY_ASSIGNED_CONTEXT ( ( #4352 ) ) GLOBAL_UNIT_ASSIGNED_CONTEXT ( ( #261, #26672, #12356 ) ) REPRESENTATION_CONTEXT ( 'NONE', 'WORKASPACE' ) );
#1893=AXIS2_PLACEMENT_3D ( 'NONE', #15878, #8621, #6738 ) ;
#1941=FACE_OUTER_BOUND ( 'NONE', #25354, .T. ) ;
#1967=ORIENTED_EDGE ( 'NONE', *, *, #25601, .F. ) ;
#2001=CARTESIAN_POINT ( 'NONE',  ( -7.783406290388187543, 3.155933242387642057, -42.35622648219886344 ) ) ;
#2036=CARTESIAN_POINT ( 'NONE',  ( 4.638687372303287759, 5.146895567816208938, -43.32728369091725540 ) ) ;
#2056=ORIENTED_EDGE ( 'NONE', *, *, #26704, .F. ) ;
#2072=CARTESIAN_POINT ( 'NONE',  ( -6.661312627754254478, -7.245008774417666331, -33.94554228739334434 ) ) ;
#2088=ORIENTED_EDGE ( 'NONE', *, *, #11772, .T. ) ;
#2134=CARTESIAN_POINT ( 'NONE',  ( 3.861721477338983632, 0.2146938847481238977, -40.92168819670553148 ) ) ;
#2147=VECTOR ( 'NONE', #28800, 1000.000000000000000 ) ;
#2229=CARTESIAN_POINT ( 'NONE',  ( -4.861312627774928785, -9.411244188027135138, -32.88899868167055018 ) ) ;
#2246=CARTESIAN_POINT ( 'NONE',  ( 7.557678206131123844, -6.153726849708399449, -34.47779604538695253 ) ) ;
#2279=ORIENTED_EDGE ( 'NONE', *, *, #17209, .F. ) ;
#2288=CARTESIAN_POINT ( 'NONE',  ( 4.638687372223567529, -9.716283825201511348, -32.74022090981630839 ) ) ;
#2322=CYLINDRICAL_SURFACE ( 'NONE', #1652, 3.000000000000003553 ) ;
#2328=CARTESIAN_POINT ( 'NONE',  ( -7.861312627709997614, 3.765626869335708449, -39.31578811167678111 ) ) ;
#2329=ORIENTED_EDGE ( 'NONE', *, *, #23249, .T. ) ;
#2341=LINE ( 'NONE', #26253, #30023 ) ;
#2361=CARTESIAN_POINT ( 'NONE',  ( 1.638687372170419598, -20.50181238077955470, -27.47976714835314738 ) ) ;
#2362=CARTESIAN_POINT ( 'NONE',  ( -0.1113126277332136399, -3.273367579602823429, -37.55154403890800552 ) ) ;
#2369=CARTESIAN_POINT ( 'NONE',  ( -5.861312627756135818, -5.597492073868338025, -34.74908987245776615 ) ) ;
#2371=ORIENTED_EDGE ( 'NONE', *, *, #18259, .T. ) ;
#2377=ORIENTED_EDGE ( 'NONE', *, *, #7334, .T. ) ;
#2396=CARTESIAN_POINT ( 'NONE',  ( 7.638687372242944029, -5.784297784966613065, -34.65797863942491830 ) ) ;
#2447=( LENGTH_UNIT ( ) NAMED_UNIT ( * ) SI_UNIT ( .MILLI., .METRE. ) );
#2485=ADVANCED_FACE ( 'NONE', ( #28609 ), #1715, .F. ) ;
#2534=CARTESIAN_POINT ( 'NONE',  ( -4.909305965083425427, -9.106205312618326886, -33.03777608198690530 ) ) ;
#2587=EDGE_LOOP ( 'NONE', ( #8612, #16649, #27006, #22613, #16346, #29631 ) ) ;
#2602=DIRECTION ( 'NONE',  ( -4.428977494234582379E-12, -0.8987940462991651502, 0.4383711467890810676 ) ) ;
#2604=CARTESIAN_POINT ( 'NONE',  ( -4.858207114627580481, -18.06692763756964482, -28.66733978701845231 ) ) ;
#2607=ORIENTED_EDGE ( 'NONE', *, *, #7583, .T. ) ;
#2627=CARTESIAN_POINT ( 'NONE',  ( 0.000000000000000000, 0.000000000000000000, 0.000000000000000000 ) ) ;
#2652=CARTESIAN_POINT ( 'NONE',  ( -0.1113126274910280905, 46.88748299613427406, -63.68552844559068404 ) ) ;
#2658=CARTESIAN_POINT ( 'NONE',  ( -4.861312627818040966, -19.47514616053552317, -31.31831154297147535 ) ) ;
#2684=CARTESIAN_POINT ( 'NONE',  ( -0.1113126277255015173, -0.6952657331094624915, -40.47787123679744070 ) ) ;
#2714=CARTESIAN_POINT ( 'NONE',  ( -4.861312627696710464, 6.462009008221268225, -40.63090155203819620 ) ) ;
#2747=CARTESIAN_POINT ( 'NONE',  ( -7.246551124551907641, 5.407433690575946805, -40.11655080252537431 ) ) ;
#2752=CARTESIAN_POINT ( 'NONE',  ( 3.790136060690228792, 1.782282071276910962, -38.34844621930091790 ) ) ;
#2815=CARTESIAN_POINT ( 'NONE',  ( -4.861312627816293919, -19.12054368222343470, -31.49126272763050238 ) ) ;
#2854=EDGE_CURVE ( 'NONE', #9948, #26056, #11611, .T. ) ;
#2857=ORIENTED_EDGE ( 'NONE', *, *, #9107, .F. ) ;
#2871=B_SPLINE_CURVE_WITH_KNOTS ( 'NONE', 3,
 ( #12471, #14543, #26490, #14388 ),
 .UNSPECIFIED., .F., .F.,
 ( 4, 4 ),
 ( 0.000000000000000000, 1.000000000000000000 ),
 .UNSPECIFIED. ) ;
#2874=CARTESIAN_POINT ( 'NONE',  ( 7.610733143571420278, -7.258930934320984463, -37.27655781773084698 ) ) ;
#2910=DIRECTION ( 'NONE',  ( -5.962915006522622422E-16, -0.4383711467890810676, -0.8987940462991651502 ) ) ;
#2933=ORIENTED_EDGE ( 'NONE', *, *, #11376, .T. ) ;
#2961=EDGE_CURVE ( 'NONE', #8590, #22717, #30442, .T. ) ;
#2980=ORIENTED_EDGE ( 'NONE', *, *, #24318, .F. ) ;
#2981=ORIENTED_EDGE ( 'NONE', *, *, #14905, .F. ) ;
#2991=CARTESIAN_POINT ( 'NONE',  ( 3.760007715734311251, -19.71206033701148996, -27.86495495698533986 ) ) ;
#2993=DIRECTION ( 'NONE',  ( -1.000000000000000000, 3.980999999999999294E-12, -1.940999999999999504E-12 ) ) ;
#3008=CARTESIAN_POINT ( 'NONE',  ( -4.861312627709997614, 3.765626869323773995, -39.31578811167095466 ) ) ;
#3009=CARTESIAN_POINT ( 'NONE',  ( -3.791072893346491224, -19.87502547375133588, -27.78547154899721150 ) ) ;
#3012=CYLINDRICAL_SURFACE ( 'NONE', #10224, 1.999999999999999778 ) ;
#3033=CARTESIAN_POINT ( 'NONE',  ( 3.941323043105160018, -19.53988727930733305, -27.94892936810068207 ) ) ;
#3069=CARTESIAN_POINT ( 'NONE',  ( 4.638687372170419820, -20.50181238079150248, -27.47976714834732448 ) ) ;
#3110=LINE ( 'NONE', #15079, #29240 ) ;
#3183=CARTESIAN_POINT ( 'NONE',  ( 3.760007715734309475, -21.02717377737872795, -30.56133709588283409 ) ) ;
#3191=CARTESIAN_POINT ( 'NONE',  ( 1.850829058368554492, -3.930924299794261056, -38.89973510835294235 ) ) ;
#3198=AXIS2_PLACEMENT_3D ( 'NONE', #4562, #14164, #7076 ) ;
#3204=AXIS2_PLACEMENT_3D ( 'NONE', #4144, #29948, #20830 ) ;
#3215=EDGE_LOOP ( 'NONE', ( #18346, #21716, #4956, #11760 ) ) ;
#3264=DIRECTION ( 'NONE',  ( -5.962915006522622422E-16, -0.4383711467890810676, -0.8987940462991651502 ) ) ;
#3309=EDGE_CURVE ( 'NONE', #18028, #9520, #10634, .T. ) ;
#3314=DIRECTION ( 'NONE',  ( -4.428977494234582379E-12, -0.8987940462991651502, 0.4383711467890810676 ) ) ;
#3335=LINE ( 'NONE', #29623, #28293 ) ;
#3432=ORIENTED_EDGE ( 'NONE', *, *, #18671, .F. ) ;
#3498=CARTESIAN_POINT ( 'NONE',  ( 3.466622106789775337, -2.539914255570844936, -39.57817603794315886 ) ) ;
#3507=VERTEX_POINT ( 'NONE', #2991 ) ;
#3508=EDGE_LOOP ( 'NONE', ( #29210, #24154, #17679, #13545 ) ) ;
#3549=CARTESIAN_POINT ( 'NONE',  ( 3.565893352360864466, 0.9842897974745647982, -41.29704520336932916 ) ) ;
#3555=B_SPLINE_CURVE_WITH_KNOTS ( 'NONE', 5,
 ( #5361, #24248, #5053, #17157, #4481, #7713, #28970, #23381, #21738, #26764, #21007, #26925 ),
 .UNSPECIFIED., .F., .F.,
 ( 6, 3, 3, 6 ),
 ( 3.339306056609999906, 4.810258468679999844, 6.613963843700000567, 6.678484287649999018 ),
 .UNSPECIFIED. ) ;
#3558=CARTESIAN_POINT ( 'NONE',  ( -3.790556161138087354, 0.9809627197493214767, -41.29542247913801845 ) ) ;
#3563=EDGE_CURVE ( 'NONE', #8967, #11921, #26751, .T. ) ;
#3612=CARTESIAN_POINT ( 'NONE',  ( 3.861721477338983632, 0.2146938849234697466, -40.92168819634601107 ) ) ;
#3633=CARTESIAN_POINT ( 'NONE',  ( -5.665412366707123226, 6.378525563588088865, -40.59018395548486069 ) ) ;
#3650=CARTESIAN_POINT ( 'NONE',  ( 4.706785070836938090, -9.032362236610094186, -33.07379175659606574 ) ) ;
#3698=VECTOR ( 'NONE', #19691, 1000.000000000000114 ) ;
#3713=ORIENTED_EDGE ( 'NONE', *, *, #26507, .T. ) ;
#3720=B_SPLINE_CURVE_WITH_KNOTS ( 'NONE', 3,
 ( #29824, #29980, #25115, #27166, #5600, #27464, #15833, #3549, #29679, #898 ),
 .UNSPECIFIED., .F., .F.,
 ( 4, 2, 2, 2, 4 ),
 ( 0.000000000000000000, 0.2500000000000000000, 0.5000000000000000000, 0.7500000000000000000, 1.000000000000000000 ),
 .UNSPECIFIED. ) ;
#3737=CARTESIAN_POINT ( 'NONE',  ( -4.861312627696711353, 5.804452288037651009, -41.97909262148694154 ) ) ;
#3740=CARTESIAN_POINT ( 'NONE',  ( -7.508028841131164199, -6.618005260559139735, -34.25135233424746417 ) ) ;
#3742=EDGE_CURVE ( 'NONE', #20431, #27935, #4542, .T. ) ;
#3747=ORIENTED_EDGE ( 'NONE', *, *, #19281, .T. ) ;
#3901=CARTESIAN_POINT ( 'NONE',  ( 7.040872694808040677, 5.396991261850427435, -40.11145768973216974 ) ) ;
#3948=VERTEX_POINT ( 'NONE', #13188 ) ;
#3970=CARTESIAN_POINT ( 'NONE',  ( -1.092383470327443540, -2.615810859415299117, -36.20335296946116443 ) ) ;
#3985=FACE_OUTER_BOUND ( 'NONE', #22993, .T. ) ;
#4027=CARTESIAN_POINT ( 'NONE',  ( 1.071322544592021586, 4.175463484545726800, -39.51567878490223507 ) ) ;
#4029=ORIENTED_EDGE ( 'NONE', *, *, #28216, .T. ) ;
#4095=ORIENTED_EDGE ( 'NONE', *, *, #25331, .F. ) ;
#4097=CARTESIAN_POINT ( 'NONE',  ( 3.391070341234815988, -1.345564551309325063, -36.82289348942992291 ) ) ;
#4098=EDGE_CURVE ( 'NONE', #4224, #97, #14158, .T. ) ;
#4100=ORIENTED_EDGE ( 'NONE', *, *, #13851, .F. ) ;
#4106=DIRECTION ( 'NONE',  ( 1.000000000000000000, -3.981000000000000101E-12, 1.940999999999999908E-12 ) ) ;
#4133=ORIENTED_EDGE ( 'NONE', *, *, #22688, .T. ) ;
#4144=CARTESIAN_POINT ( 'NONE',  ( -0.1113126277255008650, -0.6952657331094624915, -40.47787123679744070 ) ) ;
#4184=EDGE_LOOP ( 'NONE', ( #19153, #6307, #31003, #10149 ) ) ;
#4224=VERTEX_POINT ( 'NONE', #10349 ) ;
#4227=ORIENTED_EDGE ( 'NONE', *, *, #23844, .F. ) ;
#4234=DIRECTION ( 'NONE',  ( 5.962915006522622422E-16, 0.4383711467890810676, 0.8987940462991651502 ) ) ;
#4248=AXIS2_PLACEMENT_3D ( 'NONE', #13738, #22874, #30583 ) ;
#4275=CARTESIAN_POINT ( 'NONE',  ( -4.888627181016710566, 6.461915854150526606, -40.63085611776214279 ) ) ;
#4291=CARTESIAN_POINT ( 'NONE',  ( 7.338008015029190645, -6.545783030477537068, -34.28657746947716589 ) ) ;
#4352=UNCERTAINTY_MEASURE_WITH_UNIT (LENGTH_MEASURE( 1.000000000000000082E-05 ), #261, 'distance_accuracy_value', 'NONE');
#4408=VERTEX_POINT ( 'NONE', #7783 ) ;
#4429=CARTESIAN_POINT ( 'NONE',  ( -6.615393565114344732, -7.263365266400284348, -33.93658922804166878 ) ) ;
#4459=ORIENTED_EDGE ( 'NONE', *, *, #24318, .T. ) ;
#4481=CARTESIAN_POINT ( 'NONE',  ( 2.881840510881505502, -20.28149510505218700, -27.58722306354944820 ) ) ;
#4491=CARTESIAN_POINT ( 'NONE',  ( -7.717292505705527716, 4.672683073074085591, -39.75818898190081541 ) ) ;
#4536=ORIENTED_EDGE ( 'NONE', *, *, #26507, .F. ) ;
#4541=CARTESIAN_POINT ( 'NONE',  ( -5.646154341209335570, 5.077040771992966661, -43.29321323052663217 ) ) ;
#4542=LINE ( 'NONE', #7054, #16590 ) ;
#4562=CARTESIAN_POINT ( 'NONE',  ( 7.638687372223567529, -9.716283825213444914, -32.74022090981047484 ) ) ;
#4605=VERTEX_POINT ( 'NONE', #13122 ) ;
#4681=EDGE_LOOP ( 'NONE', ( #29799, #13105, #7613, #8297 ) ) ;
#4761=( GEOMETRIC_REPRESENTATION_CONTEXT ( 3 ) GLOBAL_UNCERTAINTY_ASSIGNED_CONTEXT ( ( #28579 ) ) GLOBAL_UNIT_ASSIGNED_CONTEXT ( ( #2447, #12037, #19587 ) ) REPRESENTATION_CONTEXT ( 'NONE', 'WORKASPACE' ) );
#4786=ORIENTED_EDGE ( 'NONE', *, *, #28216, .F. ) ;
#4787=EDGE_CURVE ( 'NONE', #4408, #6144, #2871, .T. ) ;
#4801=ORIENTED_EDGE ( 'NONE', *, *, #24644, .T. ) ;
#4879=ORIENTED_EDGE ( 'NONE', *, *, #18466, .F. ) ;
#4928=CARTESIAN_POINT ( 'NONE',  ( 7.499725500497901542, -7.593926722894613235, -37.11316945461116035 ) ) ;
#4934=DIRECTION ( 'NONE',  ( -5.962915006522622422E-16, -0.4383711467890810676, -0.8987940462991651502 ) ) ;
#4956=ORIENTED_EDGE ( 'NONE', *, *, #25149, .T. ) ;
#5026=CYLINDRICAL_SURFACE ( 'NONE', #23253, 4.099999999999999645 ) ;
#5034=VERTEX_POINT ( 'NONE', #3183 ) ;
#5045=CYLINDRICAL_SURFACE ( 'NONE', #24551, 4.099999999999997868 ) ;
#5053=CARTESIAN_POINT ( 'NONE',  ( 3.453746560993067316, -19.96450010785953566, -27.74183185409264851 ) ) ;
#5080=DIRECTION ( 'NONE',  ( -4.428977494234582379E-12, -0.8987940462991651502, 0.4383711467890810676 ) ) ;
#5089=CARTESIAN_POINT ( 'NONE',  ( -7.861312627709997614, 3.765626869511068620, -39.31578811131726781 ) ) ;
#5121=DIRECTION ( 'NONE',  ( 5.962915006522622422E-16, 0.4383711467890810676, 0.8987940462991651502 ) ) ;
#5172=CYLINDRICAL_SURFACE ( 'NONE', #20802, 1.999999999999999778 ) ;
#5211=LINE ( 'NONE', #7422, #16325 ) ;
#5215=DIRECTION ( 'NONE',  ( 0.8366600265365546907, 0.4922897737059920287, -0.2401057656541278063 ) ) ;
#5227=ORIENTED_EDGE ( 'NONE', *, *, #16542, .F. ) ;
#5277=CARTESIAN_POINT ( 'NONE',  ( -4.129410714115038239, -19.58013141257310252, -27.92930099280837197 ) ) ;
#5301=CARTESIAN_POINT ( 'NONE',  ( 7.638687372291747657, 2.805115907256121144, -42.18512143522137592 ) ) ;
#5346=CARTESIAN_POINT ( 'NONE',  ( -5.702373156330470927, -9.141065521210249400, -36.35857944363798566 ) ) ;
#5361=CARTESIAN_POINT ( 'NONE',  ( 3.760007715734311251, -19.71206033701148996, -27.86495495698533986 ) ) ;
#5365=LINE ( 'NONE', #14512, #3698 ) ;
#5370=CARTESIAN_POINT ( 'NONE',  ( -2.200711091379580431, -20.50181238076427448, -27.47976714836060097 ) ) ;
#5393=CARTESIAN_POINT ( 'NONE',  ( 6.481092934035197040, 4.607732177564153098, -43.06431613492966903 ) ) ;
#5400=CARTESIAN_POINT ( 'NONE',  ( -6.661312627754254478, -7.245008774242306160, -33.94554228703383103 ) ) ;
#5448=ADVANCED_FACE ( 'NONE', ( #20565 ), #24407, .T. ) ;
#5458=CARTESIAN_POINT ( 'NONE',  ( -0.1113126277073495929, 2.989789856717120387, -42.27519293863267791 ) ) ;
#5488=EDGE_LOOP ( 'NONE', ( #27503, #15488, #8684, #8669, #23780, #8219, #19638, #22878, #8071, #6815, #24594, #14210, #22404, #28136, #3713, #2377, #24766, #18086, #2088, #25941 ) ) ;
#5506=CARTESIAN_POINT ( 'NONE',  ( 1.638687372183706747, -17.80543024188206758, -28.79488058872038891 ) ) ;
#5524=ORIENTED_EDGE ( 'NONE', *, *, #24708, .T. ) ;
#5525=CARTESIAN_POINT ( 'NONE',  ( -4.861312627776431583, -9.716283824988348528, -32.74022090947522656 ) ) ;
#5595=CARTESIAN_POINT ( 'NONE',  ( 3.861721477338985409, 1.529807325115373207, -38.22530605780803370 ) ) ;
#5598=DIRECTION ( 'NONE',  ( -5.962915006522622422E-16, -0.4383711467890810676, -0.8987940462991651502 ) ) ;
#5600=CARTESIAN_POINT ( 'NONE',  ( 2.048088563388107186, 2.463427384171473999, -42.01846880737406309 ) ) ;
#5610=CARTESIAN_POINT ( 'NONE',  ( -3.290913549170359165, 1.665752135100502684, -41.62941659330974886 ) ) ;
#5617=DIRECTION ( 'NONE',  ( -0.8366600265317032381, 0.4922897737126532003, -0.2401057656573751253 ) ) ;
#5639=VERTEX_POINT ( 'NONE', #878 ) ;
#5676=DIRECTION ( 'NONE',  ( 5.962915006522623408E-16, 0.4383711467890811231, 0.8987940462991652613 ) ) ;
#5692=CARTESIAN_POINT ( 'NONE',  ( 4.638687372223565752, -11.03139726556875999, -35.43660304871379907 ) ) ;
#5734=VECTOR ( 'NONE', #22273, 1000.000000000000000 ) ;
#5856=CARTESIAN_POINT ( 'NONE',  ( 3.861721477338983632, 0.2146938847481238977, -40.92168819670553148 ) ) ;
#5864=VERTEX_POINT ( 'NONE', #19572 ) ;
#5870=EDGE_CURVE ( 'NONE', #23873, #9948, #21938, .T. ) ;
#5950=PRODUCT_CONTEXT ( 'NONE', #26256, 'mechanical' ) ;
#6016=CARTESIAN_POINT ( 'NONE',  ( 5.112097824811119295, -8.183944344857142283, -33.48759281112634056 ) ) ;
#6017=ORIENTED_EDGE ( 'NONE', *, *, #25247, .F. ) ;
#6019=LINE ( 'NONE', #15464, #19342 ) ;
#6020=ORIENTED_EDGE ( 'NONE', *, *, #7319, .F. ) ;
#6083=DIRECTION ( 'NONE',  ( 5.962915006522623408E-16, 0.4383711467890811231, 0.8987940462991652613 ) ) ;
#6144=VERTEX_POINT ( 'NONE', #8834 ) ;
#6171=CARTESIAN_POINT ( 'NONE',  ( 2.247213954888706677, -3.736744008551091678, -38.99444316444944292 ) ) ;
#6180=CARTESIAN_POINT ( 'NONE',  ( 7.638687372243862406, -6.912605514289321462, -37.44547201132905911 ) ) ;
#6260=LINE ( 'NONE', #20902, #8769 ) ;
#6307=ORIENTED_EDGE ( 'NONE', *, *, #19701, .F. ) ;
#6385=CARTESIAN_POINT ( 'NONE',  ( 0.2854594907656595737, 4.304903296723256112, -39.57881079955906500 ) ) ;
#6398=FACE_OUTER_BOUND ( 'NONE', #4184, .T. ) ;
#6461=ORIENTED_EDGE ( 'NONE', *, *, #130, .F. ) ;
#6462=PLANE ( 'NONE',  #28029 ) ;
#6495=LINE ( 'NONE', #8531, #769 ) ;
#6535=CARTESIAN_POINT ( 'NONE',  ( -0.1113126278295802629, -20.50181238077258783, -27.47976714835654732 ) ) ;
#6565=CARTESIAN_POINT ( 'NONE',  ( -7.521481332671076103, -6.600127069647881761, -34.26007211057947899 ) ) ;
#6607=CARTESIAN_POINT ( 'NONE',  ( 2.317629466759838053, -2.355760913644644461, -36.33018780266829850 ) ) ;
#6679=CARTESIAN_POINT ( 'NONE',  ( -7.534632680830990026, -7.897185061638417380, -36.96526048005145526 ) ) ;
#6719=CARTESIAN_POINT ( 'NONE',  ( -6.851801499143887142, -7.170286489046357126, -33.98198678106104609 ) ) ;
#6733=DIRECTION ( 'NONE',  ( 1.000000000000000000, -3.980999999999999294E-12, 1.940999999999999504E-12 ) ) ;
#6738=DIRECTION ( 'NONE',  ( -0.7071067811896790678, -0.6355433650254203037, 0.3099752105697111682 ) ) ;
#6779=B_SPLINE_CURVE_WITH_KNOTS ( 'NONE', 5,
 ( #28665, #2396, #13886, #2246, #11836, #6798, #4291, #21436, #31030 ),
 .UNSPECIFIED., .F., .F.,
 ( 6, 3, 6 ),
 ( 0.000000000000000000, 1.472643962950000329, 1.642768356969999788 ),
 .UNSPECIFIED. ) ;
#6798=CARTESIAN_POINT ( 'NONE',  ( 7.350552255519282596, -6.527378230651997626, -34.29555409013811129 ) ) ;
#6815=ORIENTED_EDGE ( 'NONE', *, *, #15252, .T. ) ;
#6846=ORIENTED_EDGE ( 'NONE', *, *, #22710, .T. ) ;
#6874=LINE ( 'NONE', #11761, #17764 ) ;
#6883=CARTESIAN_POINT ( 'NONE',  ( 4.680451711962687611, -10.51223169637473376, -35.68981701567106768 ) ) ;
#6919=DIRECTION ( 'NONE',  ( -0.9690327085533227969, -0.2219413702013694756, 0.1082480389981703706 ) ) ;
#6961=CARTESIAN_POINT ( 'NONE',  ( 4.638687372183706970, -17.80543024189401535, -28.79488058871456957 ) ) ;
#6967=ORIENTED_EDGE ( 'NONE', *, *, #24708, .F. ) ;
#6975=B_SPLINE_CURVE_WITH_KNOTS ( 'NONE', 5,
 ( #1699, #6719, #10985, #23427, #16323, #21054, #3740, #6565, #30803 ),
 .UNSPECIFIED., .F., .F.,
 ( 6, 3, 6 ),
 ( 0.000000000000000000, 1.472643963329999917, 1.642768356779999994 ),
 .UNSPECIFIED. ) ;
#7047=VECTOR ( 'NONE', #27061, 1000.000000000000114 ) ;
#7048=DIRECTION ( 'NONE',  ( 4.428977494234582379E-12, 0.8987940462991651502, -0.4383711467890810676 ) ) ;
#7054=CARTESIAN_POINT ( 'NONE',  ( -1.092383471258445704, -3.930924299782534437, -38.89973510835866222 ) ) ;
#7071=CARTESIAN_POINT ( 'NONE',  ( -4.260936785125032600, -20.77695744284302037, -30.68337575642739168 ) ) ;
#7076=DIRECTION ( 'NONE',  ( 4.429038154748118518E-12, 0.8987940462991653723, -0.4383711467890809010 ) ) ;
#7180=B_SPLINE_CURVE_WITH_KNOTS ( 'NONE', 3,
 ( #5458, #19788, #12691, #17566, #20401, #15369, #5610, #3558, #15064, #12539 ),
 .UNSPECIFIED., .F., .F.,
 ( 4, 2, 2, 2, 4 ),
 ( 0.000000000000000000, 0.2500000000000000000, 0.5000000000000000000, 0.7500000000000000000, 1.000000000000000000 ),
 .UNSPECIFIED. ) ;
#7185=CARTESIAN_POINT ( 'NONE',  ( 4.638687372290002386, 3.765626869285956690, -39.31578811165251608 ) ) ;
#7226=CARTESIAN_POINT ( 'NONE',  ( -4.783592046303898115, -19.82595474192468288, -31.14721076547942147 ) ) ;
#7247=CARTESIAN_POINT ( 'NONE',  ( -4.861312627775142836, -10.76947865206767219, -35.56434929207025419 ) ) ;
#7306=LINE ( 'NONE', #5089, #21018 ) ;
#7319=EDGE_CURVE ( 'NONE', #26056, #26210, #10310, .T. ) ;
#7331=CARTESIAN_POINT ( 'NONE',  ( -4.826218213038748317, -18.30365710847786787, -28.55187910938255769 ) ) ;
#7334=EDGE_CURVE ( 'NONE', #1312, #22717, #7477, .T. ) ;
#7342=CARTESIAN_POINT ( 'NONE',  ( -4.861312627709997614, 3.765626869323773995, -39.31578811167095466 ) ) ;
#7397=CARTESIAN_POINT ( 'NONE',  ( -6.148616650685278628, -8.802192167974602910, -36.52385902140760976 ) ) ;
#7422=CARTESIAN_POINT ( 'NONE',  ( 4.638687372203635917, -15.07597047391499778, -33.46393288816293676 ) ) ;
#7466=SURFACE_STYLE_USAGE ( .BOTH. , #404 ) ;
#7477=LINE ( 'NONE', #10153, #29605 ) ;
#7479=CARTESIAN_POINT ( 'NONE',  ( -4.263497950344331322, -19.43679463443259792, -27.99921101064753159 ) ) ;
#7501=CARTESIAN_POINT ( 'NONE',  ( 7.638687372290000610, 2.450513428906772706, -42.01217025054418741 ) ) ;
#7577=CARTESIAN_POINT ( 'NONE',  ( 3.861721477338985409, 1.529807325115373207, -38.22530605780803370 ) ) ;
#7583=EDGE_CURVE ( 'NONE', #1757, #1312, #1330, .T. ) ;
#7594=CARTESIAN_POINT ( 'NONE',  ( 7.638687372242999984, -7.087249463098728164, -37.36029246609886911 ) ) ;
#7613=ORIENTED_EDGE ( 'NONE', *, *, #2961, .F. ) ;
#7653=VERTEX_POINT ( 'NONE', #23522 ) ;
#7676=CARTESIAN_POINT ( 'NONE',  ( -7.861312627776432471, -9.716283825151744935, -32.74022090984056632 ) ) ;
#7679=CARTESIAN_POINT ( 'NONE',  ( 6.438687372205746051, -7.245008774379918748, -33.94554228741176161 ) ) ;
#7707=DIRECTION ( 'NONE',  ( -0.7071067811834158556, 0.6355433650310500227, -0.3099752105724556395 ) ) ;
#7713=CARTESIAN_POINT ( 'NONE',  ( 2.442787111560830837, -20.41832893614638067, -27.52048474490649355 ) ) ;
#7723=CARTESIAN_POINT ( 'NONE',  ( -2.870505120338942007, -20.37236795256072597, -27.54290141440374384 ) ) ;
#7783=CARTESIAN_POINT ( 'NONE',  ( -7.534632680830988249, -6.582071621271182060, -34.26887834115397169 ) ) ;
#7852=CARTESIAN_POINT ( 'NONE',  ( -4.861312627796364083, -15.07597047387718092, -33.46393288818136824 ) ) ;
#7911=PRODUCT_DEFINITION ( 'UNKNOWN', '', #29425, #26674 ) ;
#7931=CARTESIAN_POINT ( 'NONE',  ( -4.861278087196373221, -17.82179692228118384, -28.78689802532309372 ) ) ;
#7980=CARTESIAN_POINT ( 'NONE',  ( -0.1113126268018901771, -2.615810859419198664, -36.20335296945926018 ) ) ;
#8010=PLANE ( 'NONE',  #18248 ) ;
#8019=CARTESIAN_POINT ( 'NONE',  ( -7.747305753407632167, -7.605135679882327970, -37.10770248100441648 ) ) ;
#8032=CARTESIAN_POINT ( 'NONE',  ( -5.861312627756135818, -5.597492073868338025, -34.74908987245776615 ) ) ;
#8033=VERTEX_POINT ( 'NONE', #2036 ) ;
#8040=EDGE_CURVE ( 'NONE', #4224, #18028, #23130, .T. ) ;
#8060=VERTEX_POINT ( 'NONE', #8788 ) ;
#8071=ORIENTED_EDGE ( 'NONE', *, *, #20909, .T. ) ;
#8113=DIRECTION ( 'NONE',  ( 5.962915006522623408E-16, 0.4383711467890811231, 0.8987940462991652613 ) ) ;
#8219=ORIENTED_EDGE ( 'NONE', *, *, #3563, .T. ) ;
#8297=ORIENTED_EDGE ( 'NONE', *, *, #29051, .T. ) ;
#8356=CARTESIAN_POINT ( 'NONE',  ( 5.032477892872088354, 5.146895567814641304, -43.32728369091649512 ) ) ;
#8383=VECTOR ( 'NONE', #22840, 1000.000000000000000 ) ;
#8435=B_SPLINE_CURVE_WITH_KNOTS ( 'NONE', 3,
 ( #11619, #23442, #16183, #18541, #16026, #19007, #18388, #6883, #23274, #11470 ),
 .UNSPECIFIED., .F., .F.,
 ( 4, 2, 2, 2, 4 ),
 ( 0.000000000000000000, 0.2500000000000000000, 0.5000000000000000000, 0.7500000000000000000, 1.000000000000000000 ),
 .UNSPECIFIED. ) ;
#8442=DIRECTION ( 'NONE',  ( -5.962915006522622422E-16, -0.4383711467890810676, -0.8987940462991651502 ) ) ;
#8454=CARTESIAN_POINT ( 'NONE',  ( -1.861312627816293253, -17.80543024186813383, -28.79488058872718881 ) ) ;
#8467=EDGE_CURVE ( 'NONE', #7653, #20431, #9914, .T. ) ;
#8483=CARTESIAN_POINT ( 'NONE',  ( -7.534632680830990026, -7.897185061638417380, -36.96526048005145526 ) ) ;
#8484=EDGE_CURVE ( 'NONE', #27419, #4224, #9405, .T. ) ;
#8500=CARTESIAN_POINT ( 'NONE',  ( -0.1113126274910263003, 48.20259643650151560, -60.98914630669319337 ) ) ;
#8525=DIRECTION ( 'NONE',  ( -5.962915006522622422E-16, -0.4383711467890810676, -0.8987940462991651502 ) ) ;
#8531=CARTESIAN_POINT ( 'NONE',  ( -4.861312627816293030, -18.46298696203981038, -30.14307165818175704 ) ) ;
#8590=VERTEX_POINT ( 'NONE', #19722 ) ;
#8612=ORIENTED_EDGE ( 'NONE', *, *, #22290, .F. ) ;
#8618=VECTOR ( 'NONE', #30274, 1000.000000000000114 ) ;
#8621=DIRECTION ( 'NONE',  ( 5.962915006522623408E-16, 0.4383711467890811231, 0.8987940462991652613 ) ) ;
#8669=ORIENTED_EDGE ( 'NONE', *, *, #20661, .T. ) ;
#8683=DIRECTION ( 'NONE',  ( 5.962915006522622422E-16, 0.4383711467890810676, 0.8987940462991651502 ) ) ;
#8684=ORIENTED_EDGE ( 'NONE', *, *, #10588, .T. ) ;
#8766=CARTESIAN_POINT ( 'NONE',  ( 7.545803529383563024, 4.488346928486736331, -39.66828223693498501 ) ) ;
#8769=VECTOR ( 'NONE', #13812, 1000.000000000000114 ) ;
#8772=ORIENTED_EDGE ( 'NONE', *, *, #27638, .T. ) ;
#8788=CARTESIAN_POINT ( 'NONE',  ( -0.1113126277073478027, 4.304903297084355707, -39.57881079973518723 ) ) ;
#8809=CARTESIAN_POINT ( 'NONE',  ( 4.638687372303289536, 6.462009008358804429, -40.63090155166024431 ) ) ;
#8834=CARTESIAN_POINT ( 'NONE',  ( -7.861312627756135818, -5.597492073231208565, -34.74908987276850780 ) ) ;
#8839=ORIENTED_EDGE ( 'NONE', *, *, #7583, .F. ) ;
#8856=B_SPLINE_CURVE_WITH_KNOTS ( 'NONE', 5,
 ( #26826, #5277, #7479, #26673, #14723, #29335, #7331, #2604, #14884, #7931, #17532, #27141 ),
 .UNSPECIFIED., .F., .F.,
 ( 6, 3, 3, 6 ),
 ( 3.339306056309999882, 4.810258468129999798, 6.613963840190000276, 6.678484286069999776 ),
 .UNSPECIFIED. ) ;
#8909=DIRECTION ( 'NONE',  ( 5.962915006522623408E-16, 0.4383711467890811231, 0.8987940462991652613 ) ) ;
#8933=EDGE_CURVE ( 'NONE', #21911, #26831, #3720, .T. ) ;
#8938=SHAPE_DEFINITION_REPRESENTATION ( #30171, #30659 ) ;
#8945=CARTESIAN_POINT ( 'NONE',  ( -6.704241792037686665, 4.607281334802888928, -43.06409624422267513 ) ) ;
#8954=CARTESIAN_POINT ( 'NONE',  ( 5.317483451773077796, 6.418870144806576583, -40.60986132251716185 ) ) ;
#8967=VERTEX_POINT ( 'NONE', #10952 ) ;
#9003=LINE ( 'NONE', #30254, #28367 ) ;
#9066=CARTESIAN_POINT ( 'NONE',  ( -7.482563026693744845, 3.808884430402179166, -42.67469205533632959 ) ) ;
#9072=B_SPLINE_CURVE_WITH_KNOTS ( 'NONE', 3,
 ( #17300, #7247, #23, #16679, #21890, #10230, #5346, #7397, #26289, #175 ),
 .UNSPECIFIED., .F., .F.,
 ( 4, 2, 2, 2, 4 ),
 ( 0.000000000000000000, 0.2500000000000000000, 0.5000000000000000000, 0.7500000000000000000, 1.000000000000000000 ),
 .UNSPECIFIED. ) ;
#9082=CARTESIAN_POINT ( 'NONE',  ( 6.906785458558747592, 5.540328039990938258, -40.18136770757133291 ) ) ;
#9094=CYLINDRICAL_SURFACE ( 'NONE', #1893, 3.000000000000003109 ) ;
#9096=CARTESIAN_POINT ( 'NONE',  ( -4.861312627696712241, 5.146895567854025799, -43.32728369093569398 ) ) ;
#9106=CARTESIAN_POINT ( 'NONE',  ( 6.666786106329811723, 5.756039377145860669, -40.28657715642490444 ) ) ;
#9107=EDGE_CURVE ( 'NONE', #8060, #22535, #1107, .T. ) ;
#9363=ORIENTED_EDGE ( 'NONE', *, *, #2854, .T. ) ;
#9405=B_SPLINE_CURVE_WITH_KNOTS ( 'NONE', 3,
 ( #21040, #30640, #2001, #9066, #18661, #1372 ),
 .UNSPECIFIED., .F., .F.,
 ( 4, 2, 4 ),
 ( 0.000000000000000000, 0.5000000000000000000, 1.000000000000000000 ),
 .UNSPECIFIED. ) ;
#9417=FACE_OUTER_BOUND ( 'NONE', #5488, .T. ) ;
#9519=CARTESIAN_POINT ( 'NONE',  ( -7.861312627708494816, 4.070676187742483521, -39.46457060538356387 ) ) ;
#9520=VERTEX_POINT ( 'NONE', #2714 ) ;
#9534=FILL_AREA_STYLE ('',( #19439 ) ) ;
#9542=LINE ( 'NONE', #16153, #13266 ) ;
#9605=DIRECTION ( 'NONE',  ( 1.000000000000000000, -3.981000000000000101E-12, 1.940999999999999908E-12 ) ) ;
#9617=LINE ( 'NONE', #12744, #2147 ) ;
#9626=EDGE_CURVE ( 'NONE', #23873, #26210, #29180, .T. ) ;
#9684=SURFACE_STYLE_USAGE ( .BOTH. , #26067 ) ;
#9705=VECTOR ( 'NONE', #20416, 1000.000000000000114 ) ;
#9785=CARTESIAN_POINT ( 'NONE',  ( -0.1113126277073503700, 2.989789856892466346, -42.27519293827315749 ) ) ;
#9786=ORIENTED_EDGE ( 'NONE', *, *, #7319, .T. ) ;
#9809=CARTESIAN_POINT ( 'NONE',  ( 7.638687372266933728, -0.9159326020094504806, -37.03243899219256008 ) ) ;
#9815=CARTESIAN_POINT ( 'NONE',  ( 3.760007715734311251, -19.71206033701148996, -27.86495495698533986 ) ) ;
#9826=ADVANCED_FACE ( 'NONE', ( #20944, #20787 ), #6462, .T. ) ;
#9830=ORIENTED_EDGE ( 'NONE', *, *, #24259, .T. ) ;
#9875=ORIENTED_EDGE ( 'NONE', *, *, #4098, .F. ) ;
#9896=CARTESIAN_POINT ( 'NONE',  ( 3.760007715734309475, -21.02717377737872795, -30.56133709588283409 ) ) ;
#9914=CIRCLE ( 'NONE', #15954, 4.100000000000000533 ) ;
#9941=CYLINDRICAL_SURFACE ( 'NONE', #14292, 3.000000000000002220 ) ;
#9948=VERTEX_POINT ( 'NONE', #26137 ) ;
#9971=CARTESIAN_POINT ( 'NONE',  ( 4.494667250129237068, -18.71248644572223796, -28.35247971844670190 ) ) ;
#9979=B_SPLINE_CURVE_WITH_KNOTS ( 'NONE', 5,
 ( #11878, #9519, #14402, #4491, #19116, #2747, #14093, #26659, #12342 ),
 .UNSPECIFIED., .F., .F.,
 ( 6, 3, 6 ),
 ( 0.000000000000000000, 2.405120303439999940, 3.339306056729999916 ),
 .UNSPECIFIED. ) ;
#9990=CARTESIAN_POINT ( 'NONE',  ( 3.233792851425277171, 2.806794219454205930, -38.84813418134861251 ) ) ;
#10012=CYLINDRICAL_SURFACE ( 'NONE', #16534, 3.000000000000001776 ) ;
#10066=EDGE_LOOP ( 'NONE', ( #22420, #15236, #28543, #22759 ) ) ;
#10102=B_SPLINE_CURVE_WITH_KNOTS ( 'NONE', 5,
 ( #25384, #1469, #22864, #15154, #6016, #15614, #3650, #22702, #27117, #1308, #10738, #17511 ),
 .UNSPECIFIED., .F., .F.,
 ( 6, 3, 3, 6 ),
 ( 0.000000000000000000, 2.408321944279999904, 4.816680746389999435, 4.935551041960000163 ),
 .UNSPECIFIED. ) ;
#10121=ORIENTED_EDGE ( 'NONE', *, *, #25043, .F. ) ;
#10127=CARTESIAN_POINT ( 'NONE',  ( 3.853224190864724896, -19.62827330940682202, -27.90582062084719439 ) ) ;
#10149=ORIENTED_EDGE ( 'NONE', *, *, #22380, .T. ) ;
#10153=CARTESIAN_POINT ( 'NONE',  ( 7.638687372266931952, -2.231046042376699567, -39.72882113109005076 ) ) ;
#10163=CARTESIAN_POINT ( 'NONE',  ( 0.8697582157755545662, -3.930924299790361509, -38.89973510835485371 ) ) ;
#10224=AXIS2_PLACEMENT_3D ( 'NONE', #8032, #5676, #5215 ) ;
#10230=CARTESIAN_POINT ( 'NONE',  ( -5.510824522656250224, -9.335491771010991258, -36.26375142553751374 ) ) ;
#10250=CARTESIAN_POINT ( 'NONE',  ( -7.003284688416608894, -8.398564518084793207, -36.72072137990513596 ) ) ;
#10264=VERTEX_POINT ( 'NONE', #19435 ) ;
#10293=CARTESIAN_POINT ( 'NONE',  ( -0.1113126277073495929, 2.989789856717120387, -42.27519293863267791 ) ) ;
#10297=CARTESIAN_POINT ( 'NONE',  ( -2.041049994039236815, 3.920024695840365503, -39.39109296326683562 ) ) ;
#10305=DIRECTION ( 'NONE',  ( 4.428977494234582379E-12, 0.8987940462991651502, -0.4383711467890810676 ) ) ;
#10310=LINE ( 'NONE', #14574, #11533 ) ;
#10349=CARTESIAN_POINT ( 'NONE',  ( -6.982632971260604116, 4.357143524085962838, -42.94209588230350505 ) ) ;
#10452=ORIENTED_EDGE ( 'NONE', *, *, #579, .T. ) ;
#10466=ORIENTED_EDGE ( 'NONE', *, *, #22013, .T. ) ;
#10533=EDGE_LOOP ( 'NONE', ( #6020, #4459, #937, #14260 ) ) ;
#10552=CARTESIAN_POINT ( 'NONE',  ( -7.861312627757861549, -7.262254661959269164, -37.27493672744613207 ) ) ;
#10588=EDGE_CURVE ( 'NONE', #16422, #16790, #17638, .T. ) ;
#10634=B_SPLINE_CURVE_WITH_KNOTS ( 'NONE', 5,
 ( #15751, #28023, #30078, #16223, #20475, #3633, #27705, #23002, #4275, #30403, #1450, #18584 ),
 .UNSPECIFIED., .F., .F.,
 ( 6, 3, 3, 6 ),
 ( 3.339306056729999916, 4.810258468379999819, 6.613963844790000657, 6.678484291160000197 ),
 .UNSPECIFIED. ) ;
#10738=CARTESIAN_POINT ( 'NONE',  ( 4.638687372223642136, -9.701227635570159435, -32.74756430415913400 ) ) ;
#10773=CARTESIAN_POINT ( 'NONE',  ( -0.1113126286645371027, -3.930924299786448195, -38.89973510835675796 ) ) ;
#10778=AXIS2_PLACEMENT_3D ( 'NONE', #5506, #6083, #7707 ) ;
#10844=ORIENTED_EDGE ( 'NONE', *, *, #2854, .F. ) ;
#10924=VECTOR ( 'NONE', #4234, 1000.000000000000114 ) ;
#10952=CARTESIAN_POINT ( 'NONE',  ( -4.861312627816293919, -19.12054368222343470, -31.49126272763050238 ) ) ;
#10985=CARTESIAN_POINT ( 'NONE',  ( -7.031490306203408203, -7.073324205343428872, -34.02927844668474222 ) ) ;
#11000=ADVANCED_FACE ( 'NONE', ( #30669 ), #9094, .T. ) ;
#11061=EDGE_LOOP ( 'NONE', ( #1555, #362, #2607, #4536 ) ) ;
#11074=EDGE_CURVE ( 'NONE', #24186, #12302, #2341, .T. ) ;
#11141=DIRECTION ( 'NONE',  ( 5.962915006522623408E-16, 0.4383711467890811231, 0.8987940462991652613 ) ) ;
#11179=VECTOR ( 'NONE', #16446, 1000.000000000000114 ) ;
#11213=VECTOR ( 'NONE', #8442, 1000.000000000000114 ) ;
#11376=EDGE_CURVE ( 'NONE', #1757, #8590, #16303, .T. ) ;
#11389=EDGE_CURVE ( 'NONE', #22717, #23873, #225, .T. ) ;
#11423=MECHANICAL_DESIGN_GEOMETRIC_PRESENTATION_REPRESENTATION('',(#869),#1877);
#11468=EDGE_LOOP ( 'NONE', ( #27974, #22177, #6846, #10121 ) ) ;
#11470=CARTESIAN_POINT ( 'NONE',  ( 4.638687372223565752, -11.03139726556875999, -35.43660304871379907 ) ) ;
#11481=CARTESIAN_POINT ( 'NONE',  ( 6.465364827590567742, 5.909465029206098841, -40.36140784685665750 ) ) ;
#11533=VECTOR ( 'NONE', #2910, 1000.000000000000114 ) ;
#11536=CARTESIAN_POINT ( 'NONE',  ( -1.861312627816293253, -17.80543024186813383, -28.79488058872718881 ) ) ;
#11611=B_SPLINE_CURVE_WITH_KNOTS ( 'NONE', 3,
 ( #23047, #23521, #21146, #16419 ),
 .UNSPECIFIED., .F., .F.,
 ( 4, 4 ),
 ( 0.000000000000000000, 1.000000000000000000 ),
 .UNSPECIFIED. ) ;
#11619=CARTESIAN_POINT ( 'NONE',  ( 6.438687372225744276, -8.560122214837054599, -36.64192442626541890 ) ) ;
#11760=ORIENTED_EDGE ( 'NONE', *, *, #3742, .F. ) ;
#11761=CARTESIAN_POINT ( 'NONE',  ( 0.8697582157835563876, -2.615810859153466783, -36.20335296958887028 ) ) ;
#11772=EDGE_CURVE ( 'NONE', #26210, #12302, #8435, .T. ) ;
#11836=CARTESIAN_POINT ( 'NONE',  ( 7.468697110890166080, -6.348049517532677655, -34.38301854759198761 ) ) ;
#11878=CARTESIAN_POINT ( 'NONE',  ( -7.861312627709997614, 3.765626869335708449, -39.31578811167678111 ) ) ;
#11899=DIRECTION ( 'NONE',  ( 5.962915006522622422E-16, 0.4383711467890810676, 0.8987940462991651502 ) ) ;
#11921=VERTEX_POINT ( 'NONE', #17108 ) ;
#11944=DIRECTION ( 'NONE',  ( -6.208823127015005183E-10, -0.4383711467890810676, -0.8987940462991651502 ) ) ;
#12017=FACE_OUTER_BOUND ( 'NONE', #26973, .T. ) ;
#12022=CARTESIAN_POINT ( 'NONE',  ( 6.760007715859398303, 5.672256964573851867, -40.24571374301982729 ) ) ;
#12037=( NAMED_UNIT ( * ) PLANE_ANGLE_UNIT ( ) SI_UNIT ( $, .RADIAN. ) );
#12040=CARTESIAN_POINT ( 'NONE',  ( 3.573234815572619905, 2.267560867816098558, -38.58513250291310470 ) ) ;
#12061=FACE_OUTER_BOUND ( 'NONE', #27276, .T. ) ;
#12121=CARTESIAN_POINT ( 'NONE',  ( -5.991145565605879852, -7.574673455881642425, -33.78475407894417515 ) ) ;
#12160=ORIENTED_EDGE ( 'NONE', *, *, #7334, .F. ) ;
#12182=CARTESIAN_POINT ( 'NONE',  ( 3.861721477338985409, 1.529807325115373207, -38.22530605780803370 ) ) ;
#12245=DIRECTION ( 'NONE',  ( 1.000000000000000000, -3.981000000000000101E-12, 1.940999999999999908E-12 ) ) ;
#12302=VERTEX_POINT ( 'NONE', #5692 ) ;
#12317=EDGE_LOOP ( 'NONE', ( #8772, #3747, #15364, #23439 ) ) ;
#12329=CARTESIAN_POINT ( 'NONE',  ( 4.638687372183706970, -17.80543024189401535, -28.79488058871456957 ) ) ;
#12331=DIRECTION ( 'NONE',  ( 5.962915006522622422E-16, 0.4383711467890810676, 0.8987940462991651502 ) ) ;
#12342=CARTESIAN_POINT ( 'NONE',  ( -6.982632971260602339, 5.672256964453205264, -40.24571374340602148 ) ) ;
#12348=CARTESIAN_POINT ( 'NONE',  ( 3.693725231361444816, 2.029077553930086708, -38.46881641890171011 ) ) ;
#12356=( NAMED_UNIT ( * ) SI_UNIT ( $, .STERADIAN. ) SOLID_ANGLE_UNIT ( ) );
#12414=FACE_OUTER_BOUND ( 'NONE', #29312, .T. ) ;
#12430=FACE_OUTER_BOUND ( 'NONE', #26665, .T. ) ;
#12471=CARTESIAN_POINT ( 'NONE',  ( -7.534632680830988249, -6.582071621271182060, -34.26887834115397169 ) ) ;
#12473=CARTESIAN_POINT ( 'NONE',  ( 4.023925869015616996, -19.44723706322411161, -27.99411789782213944 ) ) ;
#12518=LINE ( 'NONE', #19922, #17760 ) ;
#12524=ADVANCED_BREP_SHAPE_REPRESENTATION ( '', ( #836, #17722 ), #14795 ) ;
#12539=CARTESIAN_POINT ( 'NONE',  ( -4.084346732781016343, 0.2146938847797513761, -40.92168819672095736 ) ) ;
#12560=CARTESIAN_POINT ( 'NONE',  ( 4.560781034842324999, -19.82596349573488581, -31.14720649596092628 ) ) ;
#12602=CARTESIAN_POINT ( 'NONE',  ( -3.889411361886101481, -19.79584274981791125, -27.82409154391096351 ) ) ;
#12664=ADVANCED_FACE ( 'NONE', ( #26606 ), #5045, .F. ) ;
#12689=ORIENTED_EDGE ( 'NONE', *, *, #22013, .F. ) ;
#12691=CARTESIAN_POINT ( 'NONE',  ( -1.010644225189164080, 2.923099265969618443, -42.24266576417440433 ) ) ;
#12700=DIRECTION ( 'NONE',  ( 4.428977494234582379E-12, 0.8987940462991651502, -0.4383711467890810676 ) ) ;
#12744=CARTESIAN_POINT ( 'NONE',  ( -0.1113126276967109224, 6.462009008202359794, -40.63090155202897336 ) ) ;
#12803=CARTESIAN_POINT ( 'NONE',  ( -3.795860071007379766, 2.267560867935308977, -38.58513250297124131 ) ) ;
#12903=ADVANCED_FACE ( 'NONE', ( #22932 ), #25128, .T. ) ;
#12975=ORIENTED_EDGE ( 'NONE', *, *, #16901, .F. ) ;
#13003=DIRECTION ( 'NONE',  ( 0.9690327085511358796, -0.2219413702090850260, 0.1082480390019309596 ) ) ;
#13029=CYLINDRICAL_SURFACE ( 'NONE', #18303, 3.000000000000001776 ) ;
#13094=CARTESIAN_POINT ( 'NONE',  ( 3.217281813909021349, -2.884757478452711688, -39.40998476019758812 ) ) ;
#13097=DIRECTION ( 'NONE',  ( 4.428977494234582379E-12, 0.8987940462991651502, -0.4383711467890810676 ) ) ;
#13105=ORIENTED_EDGE ( 'NONE', *, *, #11389, .F. ) ;
#13109=ADVANCED_FACE ( 'NONE', ( #6398 ), #26074, .F. ) ;
#13122=CARTESIAN_POINT ( 'NONE',  ( -3.982632971385690279, -21.02717377734789039, -30.56133709589786207 ) ) ;
#13174=CARTESIAN_POINT ( 'NONE',  ( 6.760007715859396527, 4.357143524031256376, -42.94209588227683128 ) ) ;
#13188=CARTESIAN_POINT ( 'NONE',  ( -6.661312627754254478, -7.245008774417666331, -33.94554228739334434 ) ) ;
#13195=EDGE_LOOP ( 'NONE', ( #487, #17481, #4029, #27051 ) ) ;
#13217=ORIENTED_EDGE ( 'NONE', *, *, #24259, .F. ) ;
#13257=AXIS2_PLACEMENT_3D ( 'NONE', #3069, #15608, #5121 ) ;
#13266=VECTOR ( 'NONE', #11899, 1000.000000000000114 ) ;
#13336=LINE ( 'NONE', #22630, #9705 ) ;
#13530=CARTESIAN_POINT ( 'NONE',  ( -6.982632971260602339, 5.672256964453205264, -40.24571374340602148 ) ) ;
#13545=ORIENTED_EDGE ( 'NONE', *, *, #17209, .T. ) ;
#13625=CARTESIAN_POINT ( 'NONE',  ( 1.818424738700763044, 3.920024695825002681, -39.39109296325933940 ) ) ;
#13631=VERTEX_POINT ( 'NONE', #30282 ) ;
#13671=ADVANCED_FACE ( 'NONE', ( #12017 ), #26491, .F. ) ;
#13681=CARTESIAN_POINT ( 'NONE',  ( 4.638687372303289536, 6.462009008183451364, -40.63090155201975762 ) ) ;
#13696=CARTESIAN_POINT ( 'NONE',  ( 3.162589221723357991, -1.641472262613852262, -36.67856965541876946 ) ) ;
#13738=CARTESIAN_POINT ( 'NONE',  ( 1.638687372183706747, -17.80543024188206758, -28.79488058872038891 ) ) ;
#13752=ORIENTED_EDGE ( 'NONE', *, *, #26577, .F. ) ;
#13812=DIRECTION ( 'NONE',  ( -5.962915006522622422E-16, -0.4383711467890810676, -0.8987940462991651502 ) ) ;
#13851=EDGE_CURVE ( 'NONE', #8033, #26188, #27434, .T. ) ;
#13857=ORIENTED_EDGE ( 'NONE', *, *, #30558, .T. ) ;
#13882=CARTESIAN_POINT ( 'NONE',  ( -3.703718188677836753, -21.27776243144296586, -30.43911684297082232 ) ) ;
#13886=CARTESIAN_POINT ( 'NONE',  ( 7.611688852352022749, -5.971102853732826787, -34.56686771967835625 ) ) ;
#13957=DIRECTION ( 'NONE',  ( 1.000000000000000000, -3.981000000000000101E-12, 1.940999999999999908E-12 ) ) ;
#13992=DIRECTION ( 'NONE',  ( 1.000000000000000000, -3.981000000000000101E-12, 1.940999999999999908E-12 ) ) ;
#14015=DIRECTION ( 'NONE',  ( 0.000000000000000000, 0.000000000000000000, 1.000000000000000000 ) ) ;
#14040=CARTESIAN_POINT ( 'NONE',  ( -1.861312627829582400, -21.81692582113286960, -30.17614928725744150 ) ) ;
#14054=VECTOR ( 'NONE', #20680, 1000.000000000000114 ) ;
#14057=FACE_OUTER_BOUND ( 'NONE', #3215, .T. ) ;
#14079=VERTEX_POINT ( 'NONE', #15224 ) ;
#14093=CARTESIAN_POINT ( 'NONE',  ( -7.163948298641449774, 5.500083906749039464, -40.16173933229066506 ) ) ;
#14154=FACE_BOUND ( 'NONE', #19967, .T. ) ;
#14158=B_SPLINE_CURVE_WITH_KNOTS ( 'NONE', 3,
 ( #23598, #8945, #23444, #4541, #25798, #9096 ),
 .UNSPECIFIED., .F., .F.,
 ( 4, 2, 4 ),
 ( 0.000000000000000000, 0.5000000000000000000, 1.000000000000000000 ),
 .UNSPECIFIED. ) ;
#14164=DIRECTION ( 'NONE',  ( 5.962915006522623408E-16, 0.4383711467890811231, 0.8987940462991652613 ) ) ;
#14166=CARTESIAN_POINT ( 'NONE',  ( 7.638687372290000610, 2.450513428906772706, -42.01217025054418741 ) ) ;
#14168=ORIENTED_EDGE ( 'NONE', *, *, #16542, .T. ) ;
#14210=ORIENTED_EDGE ( 'NONE', *, *, #4098, .T. ) ;
#14260=ORIENTED_EDGE ( 'NONE', *, *, #11772, .F. ) ;
#14275=VECTOR ( 'NONE', #5598, 1000.000000000000114 ) ;
#14277=DIRECTION ( 'NONE',  ( 5.962915006522623408E-16, 0.4383711467890811231, 0.8987940462991652613 ) ) ;
#14292=AXIS2_PLACEMENT_3D ( 'NONE', #3008, #24721, #514 ) ;
#14339=ORIENTED_EDGE ( 'NONE', *, *, #27638, .F. ) ;
#14388=CARTESIAN_POINT ( 'NONE',  ( -7.861312627756135818, -5.597492073231208565, -34.74908987276850780 ) ) ;
#14402=CARTESIAN_POINT ( 'NONE',  ( -7.813316244716991932, 4.375724744151460399, -39.61335272743919944 ) ) ;
#14429=CARTESIAN_POINT ( 'NONE',  ( 3.150050076769718377, -21.47638757757964711, -30.34224088629133576 ) ) ;
#14438=COLOUR_RGB ( '', 0.08235294, 0.09019608, 0.10196078) ;
#14451=CARTESIAN_POINT ( 'NONE',  ( 1.850829058368556268, -2.615810859427025736, -36.20335296945545167 ) ) ;
#14467=ADVANCED_FACE ( 'NONE', ( #12061 ), #10012, .T. ) ;
#14479=EDGE_CURVE ( 'NONE', #5034, #16422, #25943, .T. ) ;
#14505=B_SPLINE_CURVE_WITH_KNOTS ( 'NONE', 5,
 ( #13681, #1728, #8954, #28155, #25329, #11481, #21082, #9106, #18706 ),
 .UNSPECIFIED., .F., .F.,
 ( 6, 3, 6 ),
 ( 0.000000000000000000, 2.405120303519999947, 3.339306056889999930 ),
 .UNSPECIFIED. ) ;
#14512=CARTESIAN_POINT ( 'NONE',  ( 4.638687372203637693, -13.76085703354776335, -30.76755074926543898 ) ) ;
#14516=FACE_OUTER_BOUND ( 'NONE', #23773, .T. ) ;
#14543=CARTESIAN_POINT ( 'NONE',  ( -7.746287188306563820, -6.291484674763839102, -34.41060706477745157 ) ) ;
#14564=B_SPLINE_CURVE_WITH_KNOTS ( 'NONE', 3,
 ( #17920, #22519, #10250, #27229, #27530, #8483 ),
 .UNSPECIFIED., .F., .F.,
 ( 4, 2, 4 ),
 ( 0.000000000000000000, 0.5000000000000000000, 1.000000000000000000 ),
 .UNSPECIFIED. ) ;
#14574=CARTESIAN_POINT ( 'NONE',  ( 6.438687372205746051, -7.245008774204572788, -33.94554228705224830 ) ) ;
#14587=CARTESIAN_POINT ( 'NONE',  ( 1.638687372170417822, -21.81692582114680334, -30.17614928725064161 ) ) ;
#14625=CARTESIAN_POINT ( 'NONE',  ( 4.038813138129719427, -20.77648683177044475, -30.68360528878402960 ) ) ;
#14627=CARTESIAN_POINT ( 'NONE',  ( -3.982632971385690279, -21.02717377734789039, -30.56133709589786207 ) ) ;
#14713=ORIENTED_EDGE ( 'NONE', *, *, #579, .F. ) ;
#14723=CARTESIAN_POINT ( 'NONE',  ( -4.616187199071799085, -18.92276888191837969, -28.24991812151081660 ) ) ;
#14740=AXIS2_PLACEMENT_3D ( 'NONE', #30616, #28553, #28234 ) ;
#14753=ORIENTED_EDGE ( 'NONE', *, *, #30558, .F. ) ;
#14795=( GEOMETRIC_REPRESENTATION_CONTEXT ( 3 ) GLOBAL_UNCERTAINTY_ASSIGNED_CONTEXT ( ( #26380 ) ) GLOBAL_UNIT_ASSIGNED_CONTEXT ( ( #93, #19119, #28864 ) ) REPRESENTATION_CONTEXT ( 'NONE', 'WORKASPACE' ) );
#14808=VECTOR ( 'NONE', #12331, 1000.000000000000114 ) ;
#14856=CARTESIAN_POINT ( 'NONE',  ( 4.590690989210701289, -18.41552811670975487, -28.49731597295215479 ) ) ;
#14864=ORIENTED_EDGE ( 'NONE', *, *, #1535, .T. ) ;
#14884=CARTESIAN_POINT ( 'NONE',  ( -4.861208984456414584, -17.82998039991930028, -28.78290667659118540 ) ) ;
#14905=EDGE_CURVE ( 'NONE', #26188, #5639, #26497, .T. ) ;
#14978=CARTESIAN_POINT ( 'NONE',  ( -3.304042416708073304, -20.19592245937915109, -27.62895963153397716 ) ) ;
#15014=EDGE_CURVE ( 'NONE', #22416, #27419, #7306, .T. ) ;
#15064=CARTESIAN_POINT ( 'NONE',  ( -3.971746973078826848, 0.6114051921346451701, -41.11517722957051291 ) ) ;
#15079=CARTESIAN_POINT ( 'NONE',  ( 1.638687372170418932, -21.15936910096317902, -28.82795821780189272 ) ) ;
#15108=CARTESIAN_POINT ( 'NONE',  ( 7.638687372236854678, -7.019901686315971112, -34.05533435017771637 ) ) ;
#15154=CARTESIAN_POINT ( 'NONE',  ( 5.571346931303373218, -7.726481253986936082, -33.71071246860980608 ) ) ;
#15167=LINE ( 'NONE', #15481, #19023 ) ;
#15224=CARTESIAN_POINT ( 'NONE',  ( -6.661312627754256255, -8.560122214784900763, -36.64192442629084212 ) ) ;
#15236=ORIENTED_EDGE ( 'NONE', *, *, #26394, .T. ) ;
#15252=EDGE_CURVE ( 'NONE', #22030, #27419, #19520, .T. ) ;
#15270=B_SPLINE_CURVE_WITH_KNOTS ( 'NONE', 3,
 ( #14627, #7071, #24216, #7226, #2658, #2815 ),
 .UNSPECIFIED., .F., .F.,
 ( 4, 2, 4 ),
 ( 0.000000000000000000, 0.5000000000000000000, 1.000000000000000000 ),
 .UNSPECIFIED. ) ;
#15364=ORIENTED_EDGE ( 'NONE', *, *, #19701, .T. ) ;
#15369=CARTESIAN_POINT ( 'NONE',  ( -2.986077861064811767, 1.962750821053097949, -41.77427253121008022 ) ) ;
#15445=CARTESIAN_POINT ( 'NONE',  ( -0.1113126278295820393, -21.81692582113983647, -30.17614928725404155 ) ) ;
#15460=CARTESIAN_POINT ( 'NONE',  ( 3.973196233977206671, -0.1784912441314041864, -40.72991899601151289 ) ) ;
#15464=CARTESIAN_POINT ( 'NONE',  ( 4.638687372183706081, -18.46298696207763967, -30.14307165816331135 ) ) ;
#15481=CARTESIAN_POINT ( 'NONE',  ( -7.861312627733067160, -0.9159326019477498360, -37.03243899222264446 ) ) ;
#15488=ORIENTED_EDGE ( 'NONE', *, *, #14479, .T. ) ;
#15535=LINE ( 'NONE', #3737, #11213 ) ;
#15580=CARTESIAN_POINT ( 'NONE',  ( 2.773968441741427426, -2.033165918578674791, -36.48752789467021529 ) ) ;
#15608=DIRECTION ( 'NONE',  ( -1.000000000000000000, 3.980999999999999294E-12, -1.940999999999999504E-12 ) ) ;
#15612=PLANE ( 'NONE',  #23261 ) ;
#15614=CARTESIAN_POINT ( 'NONE',  ( 4.811998177268387522, -8.737919599237365276, -33.21740102630603531 ) ) ;
#15617=CARTESIAN_POINT ( 'NONE',  ( -7.861312627756137594, -6.912605513598457208, -37.44547201166600559 ) ) ;
#15622=DIRECTION ( 'NONE',  ( -0.7071067811896794009, -0.6355433650254203037, 0.3099752105697101134 ) ) ;
#15643=ORIENTED_EDGE ( 'NONE', *, *, #22114, .F. ) ;
#15677=CARTESIAN_POINT ( 'NONE',  ( 5.638687372243864182, -5.597492073914120070, -34.74908987243544090 ) ) ;
#15708=B_SPLINE_CURVE_WITH_KNOTS ( 'NONE', 3,
 ( #5856, #15460, #25065, #27726, #1144, #3498, #13094, #24756, #6171, #3191 ),
 .UNSPECIFIED., .F., .F.,
 ( 4, 2, 2, 2, 4 ),
 ( 0.000000000000000000, 0.2500000000000000000, 0.5000000000000000000, 0.7500000000000000000, 1.000000000000000000 ),
 .UNSPECIFIED. ) ;
#15751=CARTESIAN_POINT ( 'NONE',  ( -6.982632971260602339, 5.672256964453205264, -40.24571374340602148 ) ) ;
#15833=CARTESIAN_POINT ( 'NONE',  ( 3.071220613210755346, 1.663153190280735494, -41.62814900322526768 ) ) ;
#15878=CARTESIAN_POINT ( 'NONE',  ( 4.638687372290002386, 3.765626869285956690, -39.31578811165251608 ) ) ;
#15879=B_SPLINE_CURVE_WITH_KNOTS ( 'NONE', 3,
 ( #27886, #28350, #18747, #25998, #13882, #18277 ),
 .UNSPECIFIED., .F., .F.,
 ( 4, 2, 4 ),
 ( 0.000000000000000000, 0.5000000000000000000, 1.000000000000000000 ),
 .UNSPECIFIED. ) ;
#15901=CARTESIAN_POINT ( 'NONE',  ( 2.011424923818943888, -2.537138457451959539, -36.24172406371944533 ) ) ;
#15954=AXIS2_PLACEMENT_3D ( 'NONE', #25918, #8909, #28113 ) ;
#16026=CARTESIAN_POINT ( 'NONE',  ( 5.288280169994311386, -9.335552363041854207, -36.26372187282946413 ) ) ;
#16073=CARTESIAN_POINT ( 'NONE',  ( -2.073454313851445630, -3.930924299778634889, -38.89973510836055937 ) ) ;
#16153=CARTESIAN_POINT ( 'NONE',  ( 3.760007715734311251, -19.71206033683614578, -27.86495495662581945 ) ) ;
#16183=CARTESIAN_POINT ( 'NONE',  ( 5.925670221678688065, -8.802561022165985349, -36.52367911919805721 ) ) ;
#16186=CARTESIAN_POINT ( 'NONE',  ( -6.982632971260602339, 5.672256964628558329, -40.24571374304650107 ) ) ;
#16211=VERTEX_POINT ( 'NONE', #578 ) ;
#16223=CARTESIAN_POINT ( 'NONE',  ( -6.505665861548826534, 6.032487712052573059, -40.42141001841366688 ) ) ;
#16227=VERTEX_POINT ( 'NONE', #24322 ) ;
#16303=LINE ( 'NONE', #9809, #18994 ) ;
#16323=CARTESIAN_POINT ( 'NONE',  ( -7.358672349382085365, -6.804754899618653319, -34.16026844937522355 ) ) ;
#16325=VECTOR ( 'NONE', #17021, 1000.000000000000114 ) ;
#16346=ORIENTED_EDGE ( 'NONE', *, *, #26394, .F. ) ;
#16418=APPLICATION_CONTEXT ( 'automotive_design' ) ;
#16419=CARTESIAN_POINT ( 'NONE',  ( 6.438687372205746051, -7.245008774379918748, -33.94554228741176161 ) ) ;
#16422=VERTEX_POINT ( 'NONE', #26038 ) ;
#16446=DIRECTION ( 'NONE',  ( -5.962915006522622422E-16, -0.4383711467890810676, -0.8987940462991651502 ) ) ;
#16516=CYLINDRICAL_SURFACE ( 'NONE', #3198, 2.999999999999999556 ) ;
#16518=FACE_OUTER_BOUND ( 'NONE', #23775, .T. ) ;
#16519=EDGE_LOOP ( 'NONE', ( #4786, #17202, #23508, #21100 ) ) ;
#16534=AXIS2_PLACEMENT_3D ( 'NONE', #7342, #19452, #24330 ) ;
#16542=EDGE_CURVE ( 'NONE', #30146, #3507, #30393, .T. ) ;
#16585=CYLINDRICAL_SURFACE ( 'NONE', #14740, 2.000000000000000444 ) ;
#16590=VECTOR ( 'NONE', #13992, 1000.000000000000000 ) ;
#16649=ORIENTED_EDGE ( 'NONE', *, *, #22688, .F. ) ;
#16658=CYLINDRICAL_SURFACE ( 'NONE', #25314, 3.000000000000000000 ) ;
#16679=CARTESIAN_POINT ( 'NONE',  ( -5.069890653733686747, -10.00948981598860854, -35.93502061437225592 ) ) ;
#16746=FILL_AREA_STYLE ('',( #16904 ) ) ;
#16780=CARTESIAN_POINT ( 'NONE',  ( 7.638583728930123939, 3.790177027337138238, -39.32776202378852304 ) ) ;
#16790=VERTEX_POINT ( 'NONE', #14040 ) ;
#16846=CARTESIAN_POINT ( 'NONE',  ( -5.732982782746885775, -7.779120688648472282, -33.68503850088168150 ) ) ;
#16901=EDGE_CURVE ( 'NONE', #9520, #20613, #9617, .T. ) ;
#16904=FILL_AREA_STYLE_COLOUR ( '', #18804 ) ;
#16936=CARTESIAN_POINT ( 'NONE',  ( 7.638687372290042354, 3.773810209576400343, -39.31977939339549266 ) ) ;
#16983=ORIENTED_EDGE ( 'NONE', *, *, #24644, .F. ) ;
#17021=DIRECTION ( 'NONE',  ( -4.428977494234582379E-12, -0.8987940462991651502, 0.4383711467890810676 ) ) ;
#17039=CARTESIAN_POINT ( 'NONE',  ( 7.418657832813924990, -7.750849174212353532, -37.03663326122587307 ) ) ;
#17108=CARTESIAN_POINT ( 'NONE',  ( -4.861312627776433359, -11.03139726553092892, -35.43660304873223765 ) ) ;
#17143=DIRECTION ( 'NONE',  ( 4.428977494234582379E-12, 0.8987940462991651502, -0.4383711467890810676 ) ) ;
#17157=CARTESIAN_POINT ( 'NONE',  ( 3.283040606112535897, -20.07229108452098032, -27.68925868202152074 ) ) ;
#17165=DIRECTION ( 'NONE',  ( -5.962915006522622422E-16, -0.4383711467890810676, -0.8987940462991651502 ) ) ;
#17175=ORIENTED_EDGE ( 'NONE', *, *, #1535, .F. ) ;
#17202=ORIENTED_EDGE ( 'NONE', *, *, #1809, .T. ) ;
#17206=ADVANCED_FACE ( 'NONE', ( #26537 ), #2322, .T. ) ;
#17209=EDGE_CURVE ( 'NONE', #7653, #24157, #21666, .T. ) ;
#17279=LINE ( 'NONE', #2362, #746 ) ;
#17290=VERTEX_POINT ( 'NONE', #30291 ) ;
#17300=CARTESIAN_POINT ( 'NONE',  ( -4.861312627776433359, -11.03139726553092892, -35.43660304873223765 ) ) ;
#17322=LINE ( 'NONE', #9785, #26374 ) ;
#17396=DIRECTION ( 'NONE',  ( 5.962915006522622422E-16, 0.4383711467890810676, 0.8987940462991651502 ) ) ;
#17473=DIRECTION ( 'NONE',  ( 5.962915006522622422E-16, 0.4383711467890810676, 0.8987940462991651502 ) ) ;
#17481=ORIENTED_EDGE ( 'NONE', *, *, #4787, .T. ) ;
#17511=CARTESIAN_POINT ( 'NONE',  ( 4.638687372223567529, -9.716283825201511348, -32.74022090981630839 ) ) ;
#17529=AXIS2_PLACEMENT_3D ( 'NONE', #15677, #20243, #5617 ) ;
#17532=CARTESIAN_POINT ( 'NONE',  ( -4.861312627816332999, -17.81361358224843627, -28.79088930694037884 ) ) ;
#17554=ADVANCED_FACE ( 'NONE', ( #19418 ), #15612, .F. ) ;
#17566=CARTESIAN_POINT ( 'NONE',  ( -1.871191271462957495, 2.657633465977181420, -42.11318944236838036 ) ) ;
#17638=LINE ( 'NONE', #15445, #8383 ) ;
#17679=ORIENTED_EDGE ( 'NONE', *, *, #8467, .F. ) ;
#17722=AXIS2_PLACEMENT_3D ( 'NONE', #2627, #14015, #29203 ) ;
#17760=VECTOR ( 'NONE', #17396, 1000.000000000000114 ) ;
#17764=VECTOR ( 'NONE', #24038, 1000.000000000000000 ) ;
#17820=ORIENTED_EDGE ( 'NONE', *, *, #25640, .F. ) ;
#17868=B_SPLINE_CURVE_WITH_KNOTS ( 'NONE', 3,
 ( #22319, #154, #12560, #28935, #14625, #9896 ),
 .UNSPECIFIED., .F., .F.,
 ( 4, 2, 4 ),
 ( 0.000000000000000000, 0.5000000000000000000, 1.000000000000000000 ),
 .UNSPECIFIED. ) ;
#17920=CARTESIAN_POINT ( 'NONE',  ( -6.661312627754256255, -8.560122214784900763, -36.64192442629084212 ) ) ;
#17951=CARTESIAN_POINT ( 'NONE',  ( 4.638687372303287759, 5.146895567816208938, -43.32728369091725540 ) ) ;
#17961=DIRECTION ( 'NONE',  ( 1.000000000000000000, -3.980999999999999294E-12, 1.940999999999999504E-12 ) ) ;
#17966=DIRECTION ( 'NONE',  ( -5.962915006522622422E-16, -0.4383711467890810676, -0.8987940462991651502 ) ) ;
#17968=DIRECTION ( 'NONE',  ( 5.962915006522623408E-16, 0.4383711467890811231, 0.8987940462991652613 ) ) ;
#18015=ORIENTED_EDGE ( 'NONE', *, *, #30993, .F. ) ;
#18028=VERTEX_POINT ( 'NONE', #13530 ) ;
#18033=AXIS2_PLACEMENT_3D ( 'NONE', #29153, #21774, #4934 ) ;
#18081=VERTEX_POINT ( 'NONE', #28311 ) ;
#18086=ORIENTED_EDGE ( 'NONE', *, *, #9626, .T. ) ;
#18132=CYLINDRICAL_SURFACE ( 'NONE', #4248, 3.000000000000002220 ) ;
#18137=CYLINDRICAL_SURFACE ( 'NONE', #3204, 4.099999999999999645 ) ;
#18155=ORIENTED_EDGE ( 'NONE', *, *, #16901, .T. ) ;
#18161=EDGE_CURVE ( 'NONE', #16227, #5034, #17868, .T. ) ;
#18248=AXIS2_PLACEMENT_3D ( 'NONE', #15108, #2993, #29728 ) ;
#18259=EDGE_CURVE ( 'NONE', #9520, #97, #15535, .T. ) ;
#18277=CARTESIAN_POINT ( 'NONE',  ( -3.982632971385690279, -21.02717377734789039, -30.56133709589786207 ) ) ;
#18303=AXIS2_PLACEMENT_3D ( 'NONE', #8454, #27657, #24848 ) ;
#18315=EDGE_CURVE ( 'NONE', #5864, #20431, #13336, .T. ) ;
#18342=CARTESIAN_POINT ( 'NONE',  ( -0.1113126277073478027, 4.304903297084355707, -39.57881079973518723 ) ) ;
#18346=ORIENTED_EDGE ( 'NONE', *, *, #18315, .F. ) ;
#18375=CARTESIAN_POINT ( 'NONE',  ( 7.603592957572457678, 4.263853735895689390, -39.55878959099714365 ) ) ;
#18388=CARTESIAN_POINT ( 'NONE',  ( 4.847509070911421247, -10.00908554550677643, -35.93521779026085028 ) ) ;
#18394=DIRECTION ( 'NONE',  ( -0.9690327085511358796, 0.2219413702090850260, -0.1082480390019309596 ) ) ;
#18437=DIRECTION ( 'NONE',  ( 1.000000000000000000, -3.981000000000000101E-12, 1.940999999999999908E-12 ) ) ;
#18466=EDGE_CURVE ( 'NONE', #17290, #10264, #8856, .T. ) ;
#18467=CARTESIAN_POINT ( 'NONE',  ( 7.638687372243864182, -5.597492073746726859, -34.74908987207204092 ) ) ;
#18498=ORIENTED_EDGE ( 'NONE', *, *, #27405, .F. ) ;
#18541=CARTESIAN_POINT ( 'NONE',  ( 5.480062667635420937, -9.140703088408896448, -36.35875621392638379 ) ) ;
#18584=CARTESIAN_POINT ( 'NONE',  ( -4.861312627696710464, 6.462009008221268225, -40.63090155203819620 ) ) ;
#18625=ADVANCED_FACE ( 'NONE', ( #12430 ), #8010, .F. ) ;
#18661=CARTESIAN_POINT ( 'NONE',  ( -7.261438393647745571, 4.106456578431311399, -42.81982768937970718 ) ) ;
#18671=EDGE_CURVE ( 'NONE', #20613, #5639, #14505, .T. ) ;
#18677=CARTESIAN_POINT ( 'NONE',  ( 7.393561943475508436, 4.882965509336187004, -39.86075057886888118 ) ) ;
#18706=CARTESIAN_POINT ( 'NONE',  ( 6.760007715859398303, 5.672256964398498802, -40.24571374337934770 ) ) ;
#18725=ORIENTED_EDGE ( 'NONE', *, *, #8484, .F. ) ;
#18747=CARTESIAN_POINT ( 'NONE',  ( -2.646164081324360762, -21.74690406887915728, -30.21030117774004964 ) ) ;
#18804=COLOUR_RGB ( '', 0.08235294, 0.09019608, 0.10196078) ;
#18880=FACE_OUTER_BOUND ( 'NONE', #10533, .T. ) ;
#18899=CARTESIAN_POINT ( 'NONE',  ( -6.630653307694315046, -7.257150041126550377, -33.93962059595295955 ) ) ;
#18970=SURFACE_STYLE_FILL_AREA ( #9534 ) ;
#18994=VECTOR ( 'NONE', #5080, 1000.000000000000114 ) ;
#19007=CARTESIAN_POINT ( 'NONE',  ( 4.969149274760951585, -9.773525261618496884, -36.05010821728498627 ) ) ;
#19023=VECTOR ( 'NONE', #10305, 1000.000000000000114 ) ;
#19035=CARTESIAN_POINT ( 'NONE',  ( -0.1113126277255008650, -0.6952657331094624915, -40.47787123679744070 ) ) ;
#19116=CARTESIAN_POINT ( 'NONE',  ( -7.520978907653607770, 5.062343813926256431, -39.94823922369914015 ) ) ;
#19119=( NAMED_UNIT ( * ) PLANE_ANGLE_UNIT ( ) SI_UNIT ( $, .RADIAN. ) );
#19153=ORIENTED_EDGE ( 'NONE', *, *, #10588, .F. ) ;
#19281=EDGE_CURVE ( 'NONE', #3507, #29499, #3555, .T. ) ;
#19307=CARTESIAN_POINT ( 'NONE',  ( 7.638687372290002386, 3.765626869274008026, -39.31578811164669673 ) ) ;
#19342=VECTOR ( 'NONE', #8525, 1000.000000000000114 ) ;
#19407=CARTESIAN_POINT ( 'NONE',  ( 7.638687372243862406, -6.912605514289321462, -37.44547201132905911 ) ) ;
#19418=FACE_OUTER_BOUND ( 'NONE', #10066, .T. ) ;
#19435=CARTESIAN_POINT ( 'NONE',  ( -4.861312627816292142, -17.80543024185618606, -28.79488058873301171 ) ) ;
#19439=FILL_AREA_STYLE_COLOUR ( '', #14438 ) ;
#19452=DIRECTION ( 'NONE',  ( 5.962915006522623408E-16, 0.4383711467890811231, 0.8987940462991652613 ) ) ;
#19465=EDGE_LOOP ( 'NONE', ( #30451, #2980, #10844, #26733, #19588, #4095, #3432, #12975, #21678, #14753, #19733, #28743, #6017, #30503, #18498, #4879, #17820, #2056, #24079, #5227 ) ) ;
#19507=VECTOR ( 'NONE', #29007, 1000.000000000000114 ) ;
#19520=LINE ( 'NONE', #24234, #20513 ) ;
#19572=CARTESIAN_POINT ( 'NONE',  ( -2.073454313851443853, -2.615810859411399569, -36.20335296946307579 ) ) ;
#19577=LINE ( 'NONE', #5400, #20823 ) ;
#19587=( NAMED_UNIT ( * ) SI_UNIT ( $, .STERADIAN. ) SOLID_ANGLE_UNIT ( ) );
#19588=ORIENTED_EDGE ( 'NONE', *, *, #11376, .F. ) ;
#19591=ORIENTED_EDGE ( 'NONE', *, *, #23249, .F. ) ;
#19609=CARTESIAN_POINT ( 'NONE',  ( 3.481616536885269841, -21.27731158793656263, -30.43933673404125173 ) ) ;
#19612=CARTESIAN_POINT ( 'NONE',  ( 7.312007425309010600, -7.897185061697537201, -36.96526048002264986 ) ) ;
#19638=ORIENTED_EDGE ( 'NONE', *, *, #157, .T. ) ;
#19664=VERTEX_POINT ( 'NONE', #7980 ) ;
#19691=DIRECTION ( 'NONE',  ( -4.428977494234582379E-12, -0.8987940462991651502, 0.4383711467890810676 ) ) ;
#19701=EDGE_CURVE ( 'NONE', #29499, #16422, #3110, .T. ) ;
#19722=CARTESIAN_POINT ( 'NONE',  ( 7.638687372243864182, -5.597492073922072819, -34.74908987243156133 ) ) ;
#19733=ORIENTED_EDGE ( 'NONE', *, *, #1809, .F. ) ;
#19746=ORIENTED_EDGE ( 'NONE', *, *, #23671, .T. ) ;
#19788=CARTESIAN_POINT ( 'NONE',  ( -0.5667420186473062227, 2.989789856359415410, -42.27519293845822546 ) ) ;
#19828=MECHANICAL_DESIGN_GEOMETRIC_PRESENTATION_REPRESENTATION('',(#30882),#4761);
#19858=CARTESIAN_POINT ( 'NONE',  ( -3.982632971385688947, -19.71206033698065596, -27.86495495700036784 ) ) ;
#19894=CARTESIAN_POINT ( 'NONE',  ( -4.012761316119771493, 1.782282071307969673, -38.34844621931605957 ) ) ;
#19922=CARTESIAN_POINT ( 'NONE',  ( -3.982632971385688947, -19.71206033680530822, -27.86495495664085098 ) ) ;
#19967=EDGE_LOOP ( 'NONE', ( #24224, #19746, #27659, #23270, #10452, #28762 ) ) ;
#20002=DIRECTION ( 'NONE',  ( -5.962915006522622422E-16, -0.4383711467890810676, -0.8987940462991651502 ) ) ;
#20062=EDGE_LOOP ( 'NONE', ( #2981, #4100, #19591, #25362 ) ) ;
#20228=CARTESIAN_POINT ( 'NONE',  ( 1.850829058368555380, -3.273367579610636291, -37.55154403890418990 ) ) ;
#20243=DIRECTION ( 'NONE',  ( 5.962915006522623408E-16, 0.4383711467890811231, 0.8987940462991652613 ) ) ;
#20335=DIRECTION ( 'NONE',  ( -5.962915006522622422E-16, -0.4383711467890810676, -0.8987940462991651502 ) ) ;
#20339=ORIENTED_EDGE ( 'NONE', *, *, #8040, .T. ) ;
#20391=B_SPLINE_CURVE_WITH_KNOTS ( 'NONE', 3,
 ( #29584, #8019, #10552, #27223 ),
 .UNSPECIFIED., .F., .F.,
 ( 4, 4 ),
 ( 0.000000000000000000, 1.000000000000000000 ),
 .UNSPECIFIED. ) ;
#20401=CARTESIAN_POINT ( 'NONE',  ( -2.267065256228490533, 2.465013841745427037, -42.01924257443324962 ) ) ;
#20416=DIRECTION ( 'NONE',  ( -5.962915006522622422E-16, -0.4383711467890810676, -0.8987940462991651502 ) ) ;
#20431=VERTEX_POINT ( 'NONE', #16073 ) ;
#20475=CARTESIAN_POINT ( 'NONE',  ( -6.104465766177795238, 6.241691732493892530, -40.52344563684190604 ) ) ;
#20477=EDGE_CURVE ( 'NONE', #13631, #3948, #26742, .T. ) ;
#20492=CARTESIAN_POINT ( 'NONE',  ( 0.8697582157755545662, -3.930924299790361509, -38.89973510835485371 ) ) ;
#20513=VECTOR ( 'NONE', #17143, 1000.000000000000114 ) ;
#20565=FACE_OUTER_BOUND ( 'NONE', #12317, .T. ) ;
#20587=ORIENTED_EDGE ( 'NONE', *, *, #24428, .T. ) ;
#20613=VERTEX_POINT ( 'NONE', #30717 ) ;
#20618=CARTESIAN_POINT ( 'NONE',  ( 3.930748841427598173, 1.248291629424108651, -38.08800167882662890 ) ) ;
#20655=B_SPLINE_CURVE_WITH_KNOTS ( 'NONE', 5,
 ( #24761, #1008, #29783, #22248, #10297, #25071, #22709, #22099, #12803, #854, #19894, #29477 ),
 .UNSPECIFIED., .F., .F.,
 ( 6, 3, 3, 6 ),
 ( 0.000000000000000000, 2.812352518870000040, 5.624713923559999884, 7.679355242909999824 ),
 .UNSPECIFIED. ) ;
#20661=EDGE_CURVE ( 'NONE', #16790, #4605, #15879, .T. ) ;
#20680=DIRECTION ( 'NONE',  ( -5.962915006522622422E-16, -0.4383711467890810676, -0.8987940462991651502 ) ) ;
#20711=ORIENTED_EDGE ( 'NONE', *, *, #22380, .F. ) ;
#20736=CARTESIAN_POINT ( 'NONE',  ( 7.160801144637284565, 5.243561765918017592, -40.03662512451870015 ) ) ;
#20777=CARTESIAN_POINT ( 'NONE',  ( 4.006917070325392238, 0.8005523405751613364, -37.86962463647368082 ) ) ;
#20787=FACE_OUTER_BOUND ( 'NONE', #19465, .T. ) ;
#20802=AXIS2_PLACEMENT_3D ( 'NONE', #2369, #28780, #21881 ) ;
#20815=PLANE ( 'NONE',  #25360 ) ;
#20823=VECTOR ( 'NONE', #22095, 1000.000000000000114 ) ;
#20830=DIRECTION ( 'NONE',  ( 0.9690327085533227969, 0.2219413702013694756, -0.1082480389981703706 ) ) ;
#20868=LINE ( 'NONE', #6535, #710 ) ;
#20902=CARTESIAN_POINT ( 'NONE',  ( -1.861312627829580402, -20.50181238059027677, -27.47976714800043041 ) ) ;
#20909=EDGE_CURVE ( 'NONE', #24098, #22030, #20391, .T. ) ;
#20911=ORIENTED_EDGE ( 'NONE', *, *, #11074, .F. ) ;
#20944=FACE_BOUND ( 'NONE', #2587, .T. ) ;
#20945=ORIENTED_EDGE ( 'NONE', *, *, #9626, .F. ) ;
#21007=CARTESIAN_POINT ( 'NONE',  ( 1.647792172260419852, -20.50181238077959733, -27.47976714835313317 ) ) ;
#21018=VECTOR ( 'NONE', #24289, 1000.000000000000114 ) ;
#21040=CARTESIAN_POINT ( 'NONE',  ( -7.861312627709999390, 2.450513428968473129, -42.01217025057427179 ) ) ;
#21054=CARTESIAN_POINT ( 'NONE',  ( -7.494278858881251892, -6.635700603326244007, -34.24272173891409210 ) ) ;
#21059=ADVANCED_FACE ( 'NONE', ( #14154, #9417 ), #21548, .F. ) ;
#21073=AXIS2_PLACEMENT_3D ( 'NONE', #25611, #21189, #13957 ) ;
#21082=CARTESIAN_POINT ( 'NONE',  ( 6.568447637800200134, 5.835222101079285295, -40.32519715133864935 ) ) ;
#21100=ORIENTED_EDGE ( 'NONE', *, *, #15252, .F. ) ;
#21146=CARTESIAN_POINT ( 'NONE',  ( 6.792853103711780527, -7.106081641748739131, -34.01330157743200289 ) ) ;
#21189=DIRECTION ( 'NONE',  ( 4.428977494234582379E-12, 0.8987940462991651502, -0.4383711467890810676 ) ) ;
#21256=VECTOR ( 'NONE', #26391, 1000.000000000000114 ) ;
#21344=VECTOR ( 'NONE', #18437, 1000.000000000000000 ) ;
#21357=DIRECTION ( 'NONE',  ( 0.7071067811896790678, 0.6355433650254203037, -0.3099752105697111126 ) ) ;
#21436=CARTESIAN_POINT ( 'NONE',  ( 7.325158325029101469, -6.564015909067758336, -34.27768470040534510 ) ) ;
#21518=CARTESIAN_POINT ( 'NONE',  ( 7.038311529316255921, 4.106927189824788549, -42.82005722189286701 ) ) ;
#21533=DIRECTION ( 'NONE',  ( -5.962915006522622422E-16, -0.4383711467890810676, -0.8987940462991651502 ) ) ;
#21548=PLANE ( 'NONE',  #1086 ) ;
#21582=CARTESIAN_POINT ( 'NONE',  ( -5.288124922799195993, -8.247920380278689123, -33.45638961376399578 ) ) ;
#21666=LINE ( 'NONE', #23881, #21256 ) ;
#21676=CARTESIAN_POINT ( 'NONE',  ( 7.560966790798962833, 3.155924488616837387, -42.35622221269955645 ) ) ;
#21678=ORIENTED_EDGE ( 'NONE', *, *, #3309, .F. ) ;
#21705=DIRECTION ( 'NONE',  ( 5.962915006522623408E-16, 0.4383711467890811231, 0.8987940462991652613 ) ) ;
#21716=ORIENTED_EDGE ( 'NONE', *, *, #28276, .T. ) ;
#21738=CARTESIAN_POINT ( 'NONE',  ( 1.666001924310420268, -20.50171922679867720, -27.47981258258537807 ) ) ;
#21774=DIRECTION ( 'NONE',  ( -4.428977494234582379E-12, -0.8987940462991651502, 0.4383711467890810676 ) ) ;
#21865=CIRCLE ( 'NONE', #22837, 4.100000000000000533 ) ;
#21881=DIRECTION ( 'NONE',  ( -0.8366600265365546907, -0.4922897737059920287, 0.2401057656541278063 ) ) ;
#21890=CARTESIAN_POINT ( 'NONE',  ( -5.191868678539384163, -9.773567673788013721, -36.05008753148776179 ) ) ;
#21911=VERTEX_POINT ( 'NONE', #10293 ) ;
#21936=CARTESIAN_POINT ( 'NONE',  ( 4.638687372182204172, -18.11047956030077799, -28.64609809500778326 ) ) ;
#21938=LINE ( 'NONE', #22090, #14808 ) ;
#21987=ADVANCED_FACE ( 'NONE', ( #30098 ), #20815, .F. ) ;
#22013=EDGE_CURVE ( 'NONE', #30146, #16227, #6019, .T. ) ;
#22022=DIRECTION ( 'NONE',  ( 1.000000000000000000, -3.981190377366772282E-12, 1.940577328459388338E-12 ) ) ;
#22030=VERTEX_POINT ( 'NONE', #15617 ) ;
#22090=CARTESIAN_POINT ( 'NONE',  ( 7.312007425309012376, -6.582071621154941710, -34.26887834076562456 ) ) ;
#22095=DIRECTION ( 'NONE',  ( -5.962915006522622422E-16, -0.4383711467890810676, -0.8987940462991651502 ) ) ;
#22099=CARTESIAN_POINT ( 'NONE',  ( -3.456418106924722622, 2.806794219390951195, -38.84813418131775364 ) ) ;
#22114=EDGE_CURVE ( 'NONE', #24098, #4408, #9003, .T. ) ;
#22124=CARTESIAN_POINT ( 'NONE',  ( 3.760007715734309475, -21.02717377737872795, -30.56133709588283409 ) ) ;
#22147=CARTESIAN_POINT ( 'NONE',  ( -0.1113126277255015173, -0.6952657331094624915, -40.47787123679744070 ) ) ;
#22177=ORIENTED_EDGE ( 'NONE', *, *, #18466, .T. ) ;
#22216=EDGE_LOOP ( 'NONE', ( #29295, #17175, #30220, #9830 ) ) ;
#22248=CARTESIAN_POINT ( 'NONE',  ( -1.293947800127978276, 4.175463484465264052, -39.51567878486299179 ) ) ;
#22273=DIRECTION ( 'NONE',  ( 1.000000000000000000, -3.981000000000000101E-12, 1.940999999999999908E-12 ) ) ;
#22289=EDGE_LOOP ( 'NONE', ( #27125, #9363, #9786, #20945 ) ) ;
#22290=EDGE_CURVE ( 'NONE', #24157, #5864, #21865, .T. ) ;
#22319=CARTESIAN_POINT ( 'NONE',  ( 4.638687372183705193, -19.12054368226126400, -31.49126272761206025 ) ) ;
#22380=EDGE_CURVE ( 'NONE', #18081, #16790, #6260, .T. ) ;
#22404=ORIENTED_EDGE ( 'NONE', *, *, #130, .T. ) ;
#22416=VERTEX_POINT ( 'NONE', #2328 ) ;
#22420=ORIENTED_EDGE ( 'NONE', *, *, #25149, .F. ) ;
#22519=CARTESIAN_POINT ( 'NONE',  ( -6.839399949238186061, -8.490264634313129832, -36.67599624484527965 ) ) ;
#22535=VERTEX_POINT ( 'NONE', #5595 ) ;
#22613=ORIENTED_EDGE ( 'NONE', *, *, #30993, .T. ) ;
#22630=CARTESIAN_POINT ( 'NONE',  ( -2.073454313851444741, -3.273367579595010124, -37.55154403891181403 ) ) ;
#22688=EDGE_CURVE ( 'NONE', #8060, #24157, #20655, .T. ) ;
#22702=CARTESIAN_POINT ( 'NONE',  ( 4.646495635265368129, -9.351076805315841511, -32.91834427498756099 ) ) ;
#22709=CARTESIAN_POINT ( 'NONE',  ( -2.998580033872426220, 3.272756371925533703, -39.07539910814716677 ) ) ;
#22710=EDGE_CURVE ( 'NONE', #10264, #8967, #6495, .T. ) ;
#22717=VERTEX_POINT ( 'NONE', #6180 ) ;
#22759=ORIENTED_EDGE ( 'NONE', *, *, #23671, .F. ) ;
#22828=CARTESIAN_POINT ( 'NONE',  ( 3.957198906281382822, -0.01292438418519503696, -37.47286552776822788 ) ) ;
#22837=AXIS2_PLACEMENT_3D ( 'NONE', #25305, #11141, #30657 ) ;
#22840=DIRECTION ( 'NONE',  ( -1.000000000000000000, 3.981000000000000101E-12, -1.940999999999999908E-12 ) ) ;
#22864=CARTESIAN_POINT ( 'NONE',  ( 5.835777567934348653, -7.528575091604372105, -33.80723775348178606 ) ) ;
#22874=DIRECTION ( 'NONE',  ( 5.962915006522623408E-16, 0.4383711467890811231, 0.8987940462991652613 ) ) ;
#22878=ORIENTED_EDGE ( 'NONE', *, *, #24709, .T. ) ;
#22932=FACE_OUTER_BOUND ( 'NONE', #22289, .T. ) ;
#22993=EDGE_LOOP ( 'NONE', ( #14339, #30628, #12689, #14168 ) ) ;
#23002=CARTESIAN_POINT ( 'NONE',  ( -5.152255138076724528, 6.459217791357691141, -40.62954018461207539 ) ) ;
#23035=ORIENTED_EDGE ( 'NONE', *, *, #2961, .T. ) ;
#23047=CARTESIAN_POINT ( 'NONE',  ( 7.312007425309012376, -6.582071621330287670, -34.26887834112514497 ) ) ;
#23130=LINE ( 'NONE', #16186, #10924 ) ;
#23235=AXIS2_PLACEMENT_3D ( 'NONE', #22147, #8113, #13003 ) ;
#23249=EDGE_CURVE ( 'NONE', #20613, #8033, #27855, .T. ) ;
#23253=AXIS2_PLACEMENT_3D ( 'NONE', #19035, #28944, #6919 ) ;
#23261=AXIS2_PLACEMENT_3D ( 'NONE', #20492, #1142, #20335 ) ;
#23270=ORIENTED_EDGE ( 'NONE', *, *, #8933, .F. ) ;
#23274=CARTESIAN_POINT ( 'NONE',  ( 4.638687372224857164, -10.76914457791739999, -35.56451223092034297 ) ) ;
#23300=CARTESIAN_POINT ( 'NONE',  ( 3.888118302228526169, 1.436696886034274812, -38.17989306233251057 ) ) ;
#23373=ADVANCED_FACE ( 'NONE', ( #18880 ), #16516, .F. ) ;
#23381=CARTESIAN_POINT ( 'NONE',  ( 1.929629880830433075, -20.49902116409572983, -27.48112851569159787 ) ) ;
#23400=VECTOR ( 'NONE', #27691, 1000.000000000000114 ) ;
#23427=CARTESIAN_POINT ( 'NONE',  ( -7.196110752422828938, -6.955782886976791701, -34.08660717815514829 ) ) ;
#23439=ORIENTED_EDGE ( 'NONE', *, *, #14479, .F. ) ;
#23442=CARTESIAN_POINT ( 'NONE',  ( 6.171604636184551573, -8.664889659197820393, -36.59082592942991141 ) ) ;
#23444=CARTESIAN_POINT ( 'NONE',  ( -6.372675331765073281, 4.806357324490649674, -43.16119209199440121 ) ) ;
#23470=EDGE_LOOP ( 'NONE', ( #1363, #26384, #14864, #25672 ) ) ;
#23508=ORIENTED_EDGE ( 'NONE', *, *, #15014, .T. ) ;
#23521=CARTESIAN_POINT ( 'NONE',  ( 7.100352917962720056, -6.872658567668013418, -34.12714961758439358 ) ) ;
#23522=CARTESIAN_POINT ( 'NONE',  ( -4.084346732781016343, 0.2146938847797513761, -40.92168819672095736 ) ) ;
#23598=CARTESIAN_POINT ( 'NONE',  ( -6.982632971260604116, 4.357143524085962838, -42.94209588230350505 ) ) ;
#23661=PLANE ( 'NONE',  #24349 ) ;
#23671=EDGE_CURVE ( 'NONE', #27935, #16211, #27564, .T. ) ;
#23702=CARTESIAN_POINT ( 'NONE',  ( 7.638687372290002386, 3.765626869274008026, -39.31578811164669673 ) ) ;
#23705=ADVANCED_FACE ( 'NONE', ( #26994 ), #24634, .F. ) ;
#23773=EDGE_LOOP ( 'NONE', ( #562, #18725, #30850, #13857 ) ) ;
#23775=EDGE_LOOP ( 'NONE', ( #20587, #13752, #18015, #6967 ) ) ;
#23780=ORIENTED_EDGE ( 'NONE', *, *, #25043, .T. ) ;
#23844=EDGE_CURVE ( 'NONE', #4605, #17290, #12518, .T. ) ;
#23873=VERTEX_POINT ( 'NONE', #19612 ) ;
#23881=CARTESIAN_POINT ( 'NONE',  ( -4.084346732781016343, 0.2146938849550972250, -40.92168819636143695 ) ) ;
#24038=DIRECTION ( 'NONE',  ( 1.000000000000000000, -3.981000000000000101E-12, 1.940999999999999908E-12 ) ) ;
#24079=ORIENTED_EDGE ( 'NONE', *, *, #19281, .F. ) ;
#24095=CARTESIAN_POINT ( 'NONE',  ( -5.005341893651962693, -8.809215901958738826, -33.18262749602455841 ) ) ;
#24098=VERTEX_POINT ( 'NONE', #6679 ) ;
#24154=ORIENTED_EDGE ( 'NONE', *, *, #18315, .T. ) ;
#24157=VERTEX_POINT ( 'NONE', #30460 ) ;
#24186=VERTEX_POINT ( 'NONE', #2288 ) ;
#24216=CARTESIAN_POINT ( 'NONE',  ( -4.482429117347703773, -20.47894748273654741, -30.82872492568852962 ) ) ;
#24224=ORIENTED_EDGE ( 'NONE', *, *, #3742, .T. ) ;
#24234=CARTESIAN_POINT ( 'NONE',  ( -7.861312627733068936, -2.231046042314999145, -39.72882113112014224 ) ) ;
#24248=CARTESIAN_POINT ( 'NONE',  ( 3.613223338493661174, -19.84398329827888219, -27.80061182959511257 ) ) ;
#24259=EDGE_CURVE ( 'NONE', #3948, #14079, #19577, .T. ) ;
#24269=CARTESIAN_POINT ( 'NONE',  ( 6.795230380966086337, -8.420262557263953340, -36.71013853908947766 ) ) ;
#24285=CARTESIAN_POINT ( 'NONE',  ( 4.298353652097317124, -19.10214718657442390, -28.16242947664836649 ) ) ;
#24289=DIRECTION ( 'NONE',  ( -5.962915006522622422E-16, -0.4383711467890810676, -0.8987940462991651502 ) ) ;
#24302=PRESENTATION_STYLE_ASSIGNMENT (( #7466 ) ) ;
#24313=PRESENTATION_STYLE_ASSIGNMENT (( #9684 ) ) ;
#24318=EDGE_CURVE ( 'NONE', #26056, #24186, #10102, .T. ) ;
#24322=CARTESIAN_POINT ( 'NONE',  ( 4.638687372183705193, -19.12054368226126400, -31.49126272761206025 ) ) ;
#24330=DIRECTION ( 'NONE',  ( 0.7071067811834159667, -0.6355433650310505778, 0.3099752105724545292 ) ) ;
#24349=AXIS2_PLACEMENT_3D ( 'NONE', #24725, #3314, #20002 ) ;
#24407=CYLINDRICAL_SURFACE ( 'NONE', #10778, 3.000000000000002220 ) ;
#24428=EDGE_CURVE ( 'NONE', #26831, #16211, #15708, .T. ) ;
#24432=CARTESIAN_POINT ( 'NONE',  ( 7.312007425309010600, -7.897185061697537201, -36.96526048002264986 ) ) ;
#24465=SHAPE_REPRESENTATION_RELATIONSHIP ( 'NONE' , 'NONE' ,  #30659, #12524 ) ;
#24551=AXIS2_PLACEMENT_3D ( 'NONE', #2684, #29114, #18394 ) ;
#24575=CARTESIAN_POINT ( 'NONE',  ( -3.687990083126857499, -19.94926840187814676, -27.74926085347921045 ) ) ;
#24594=ORIENTED_EDGE ( 'NONE', *, *, #8484, .T. ) ;
#24634=PLANE ( 'NONE',  #13257 ) ;
#24637=B_SPLINE_CURVE_WITH_KNOTS ( 'NONE', 5,
 ( #26935, #5370, #29281, #7723, #14978, #24575, #3009, #12602, #19858 ),
 .UNSPECIFIED., .F., .F.,
 ( 6, 3, 6 ),
 ( 0.000000000000000000, 2.405120302929999898, 3.339306056309999438 ),
 .UNSPECIFIED. ) ;
#24644=EDGE_CURVE ( 'NONE', #8060, #21911, #17322, .T. ) ;
#24649=AXIS2_PLACEMENT_3D ( 'NONE', #27551, #6733, #7048 ) ;
#24669=LINE ( 'NONE', #29227, #29349 ) ;
#24708=EDGE_CURVE ( 'NONE', #26831, #22535, #661, .T. ) ;
#24709=EDGE_CURVE ( 'NONE', #14079, #24098, #14564, .T. ) ;
#24721=DIRECTION ( 'NONE',  ( 5.962915006522623408E-16, 0.4383711467890811231, 0.8987940462991652613 ) ) ;
#24725=CARTESIAN_POINT ( 'NONE',  ( -1.092383471258445704, -3.930924299782534437, -38.89973510835866222 ) ) ;
#24756=CARTESIAN_POINT ( 'NONE',  ( 2.607517555921732288, -3.483231422657013354, -39.11808951420159275 ) ) ;
#24761=CARTESIAN_POINT ( 'NONE',  ( -0.1113126277073478027, 4.304903297084355707, -39.57881079973518723 ) ) ;
#24766=ORIENTED_EDGE ( 'NONE', *, *, #11389, .T. ) ;
#24848=DIRECTION ( 'NONE',  ( 0.7071067811896794009, 0.6355433650254204148, -0.3099752105697101690 ) ) ;
#24910=DIRECTION ( 'NONE',  ( -5.962915006522622422E-16, -0.4383711467890810676, -0.8987940462991651502 ) ) ;
#24999=EDGE_LOOP ( 'NONE', ( #1967, #20911, #786, #10466 ) ) ;
#25043=EDGE_CURVE ( 'NONE', #4605, #8967, #15270, .T. ) ;
#25065=CARTESIAN_POINT ( 'NONE',  ( 4.011748363780728077, -0.5882954696724371768, -40.53004412028315784 ) ) ;
#25071=CARTESIAN_POINT ( 'NONE',  ( -2.698832034861248896, 3.511840374587876568, -39.19200816765035000 ) ) ;
#25115=CARTESIAN_POINT ( 'NONE',  ( 0.7914749696353690078, 2.922173311402426865, -42.24221414595644575 ) ) ;
#25128=CYLINDRICAL_SURFACE ( 'NONE', #17529, 2.000000000000000444 ) ;
#25149=EDGE_CURVE ( 'NONE', #19664, #27935, #17279, .T. ) ;
#25245=CARTESIAN_POINT ( 'NONE',  ( 7.638687372290001498, 3.108070149090397472, -40.66397918109543497 ) ) ;
#25247=EDGE_CURVE ( 'NONE', #3948, #4408, #6975, .T. ) ;
#25305=CARTESIAN_POINT ( 'NONE',  ( -0.1113126277254997409, 0.6198477072577868174, -37.78148909789995002 ) ) ;
#25314=AXIS2_PLACEMENT_3D ( 'NONE', #7676, #21705, #22022 ) ;
#25329=CARTESIAN_POINT ( 'NONE',  ( 6.081417161111781766, 6.156119086796980611, -40.48170906884572418 ) ) ;
#25331=EDGE_CURVE ( 'NONE', #5639, #1757, #28374, .T. ) ;
#25349=CARTESIAN_POINT ( 'NONE',  ( 2.167139767879371348, -2.450417181414907386, -36.28402085616472306 ) ) ;
#25354=EDGE_LOOP ( 'NONE', ( #4227, #30932, #20711, #26591 ) ) ;
#25360=AXIS2_PLACEMENT_3D ( 'NONE', #1148, #17961, #13097 ) ;
#25362=ORIENTED_EDGE ( 'NONE', *, *, #18671, .T. ) ;
#25384=CARTESIAN_POINT ( 'NONE',  ( 6.438687372205746051, -7.245008774379918748, -33.94554228741176161 ) ) ;
#25467=CARTESIAN_POINT ( 'NONE',  ( 6.760007715859398303, 5.672256964398498802, -40.24571374337934770 ) ) ;
#25594=CARTESIAN_POINT ( 'NONE',  ( 0.6822309889224468238, 4.261764438830168089, -39.55777057273109421 ) ) ;
#25601=EDGE_CURVE ( 'NONE', #12302, #16227, #5211, .T. ) ;
#25611=CARTESIAN_POINT ( 'NONE',  ( -4.861312627829579291, -20.50181238075367318, -27.47976714836577017 ) ) ;
#25640=EDGE_CURVE ( 'NONE', #18081, #17290, #24637, .T. ) ;
#25667=CARTESIAN_POINT ( 'NONE',  ( 3.911140671018063397, 1.342814479487780543, -38.13410355316680977 ) ) ;
#25672=ORIENTED_EDGE ( 'NONE', *, *, #3563, .F. ) ;
#25707=B_SPLINE_CURVE_WITH_KNOTS ( 'NONE', 3,
 ( #29057, #21518, #28905, #21676, #5301, #7501 ),
 .UNSPECIFIED., .F., .F.,
 ( 4, 2, 4 ),
 ( 0.000000000000000000, 0.5000000000000000000, 1.000000000000000000 ),
 .UNSPECIFIED. ) ;
#25798=CARTESIAN_POINT ( 'NONE',  ( -5.255844033138538762, 5.146895567855596987, -43.32728369093645426 ) ) ;
#25833=CARTESIAN_POINT ( 'NONE',  ( -4.861312627696712241, 5.146895567854025799, -43.32728369093569398 ) ) ;
#25916=CARTESIAN_POINT ( 'NONE',  ( 7.312007425309010600, -7.897185061697537201, -36.96526048002264986 ) ) ;
#25918=CARTESIAN_POINT ( 'NONE',  ( -0.1113126277255015173, -0.6952657331094624915, -40.47787123679744070 ) ) ;
#25941=ORIENTED_EDGE ( 'NONE', *, *, #25601, .T. ) ;
#25943=B_SPLINE_CURVE_WITH_KNOTS ( 'NONE', 3,
 ( #22124, #19609, #14429, #584, #29189, #14587 ),
 .UNSPECIFIED., .F., .F.,
 ( 4, 2, 4 ),
 ( 0.000000000000000000, 0.5000000000000000000, 1.000000000000000000 ),
 .UNSPECIFIED. ) ;
#25998=CARTESIAN_POINT ( 'NONE',  ( -3.372638840113360459, -21.47650793462416630, -30.34218218423842472 ) ) ;
#26038=CARTESIAN_POINT ( 'NONE',  ( 1.638687372170417822, -21.81692582114680334, -30.17614928725064161 ) ) ;
#26056=VERTEX_POINT ( 'NONE', #7679 ) ;
#26067=SURFACE_SIDE_STYLE ('',( #18970 ) ) ;
#26074=PLANE ( 'NONE',  #21073 ) ;
#26137=CARTESIAN_POINT ( 'NONE',  ( 7.312007425309012376, -6.582071621330287670, -34.26887834112514497 ) ) ;
#26188=VERTEX_POINT ( 'NONE', #13174 ) ;
#26210=VERTEX_POINT ( 'NONE', #29709 ) ;
#26253=CARTESIAN_POINT ( 'NONE',  ( 4.638687372223566641, -10.37384054538513567, -34.08841197926504663 ) ) ;
#26256=APPLICATION_CONTEXT ( 'automotive_design' ) ;
#26289=CARTESIAN_POINT ( 'NONE',  ( -6.393889225687406253, -8.665023291132417427, -36.59076075278051832 ) ) ;
#26374=VECTOR ( 'NONE', #17165, 1000.000000000000114 ) ;
#26380=UNCERTAINTY_MEASURE_WITH_UNIT (LENGTH_MEASURE( 1.000000000000000082E-05 ), #93, 'distance_accuracy_value', 'NONE');
#26384=ORIENTED_EDGE ( 'NONE', *, *, #27405, .T. ) ;
#26391=DIRECTION ( 'NONE',  ( 5.962915006522622422E-16, 0.4383711467890810676, 0.8987940462991651502 ) ) ;
#26394=EDGE_CURVE ( 'NONE', #19664, #528, #6874, .T. ) ;
#26451=CARTESIAN_POINT ( 'NONE',  ( -6.292028302495006109, -7.397523702828756598, -33.87115578656446502 ) ) ;
#26490=CARTESIAN_POINT ( 'NONE',  ( -7.861312627893095595, -5.944809905196246191, -34.57969164752912405 ) ) ;
#26491=PLANE ( 'NONE',  #18033 ) ;
#26497=LINE ( 'NONE', #12022, #19507 ) ;
#26507=EDGE_CURVE ( 'NONE', #26188, #1312, #25707, .T. ) ;
#26510=SURFACE_STYLE_FILL_AREA ( #16746 ) ;
#26513=CARTESIAN_POINT ( 'NONE',  ( 2.775954778257573530, 3.272756372082325171, -39.07539910822363538 ) ) ;
#26537=FACE_OUTER_BOUND ( 'NONE', #20062, .T. ) ;
#26577=EDGE_CURVE ( 'NONE', #528, #16211, #27314, .T. ) ;
#26591=ORIENTED_EDGE ( 'NONE', *, *, #25640, .T. ) ;
#26598=CARTESIAN_POINT ( 'NONE',  ( -0.1113126276967127126, 5.146895567835117369, -43.32728369092647824 ) ) ;
#26606=FACE_OUTER_BOUND ( 'NONE', #3508, .T. ) ;
#26659=CARTESIAN_POINT ( 'NONE',  ( -7.075849446371014650, 5.588469936758675871, -40.20484807950032291 ) ) ;
#26665=EDGE_LOOP ( 'NONE', ( #12160, #8839, #2933, #23035 ) ) ;
#26672=( NAMED_UNIT ( * ) PLANE_ANGLE_UNIT ( ) SI_UNIT ( $, .RADIAN. ) );
#26673=CARTESIAN_POINT ( 'NONE',  ( -4.383426400183576099, -19.28336513850018008, -28.07404357586100829 ) ) ;
#26674=PRODUCT_DEFINITION_CONTEXT ( 'detailed design', #16418, 'design' ) ;
#26704=EDGE_CURVE ( 'NONE', #29499, #18081, #20868, .T. ) ;
#26733=ORIENTED_EDGE ( 'NONE', *, *, #29051, .F. ) ;
#26742=B_SPLINE_CURVE_WITH_KNOTS ( 'NONE', 5,
 ( #180, #2229, #2534, #24095, #21582, #16846, #12121, #26451, #4429, #18899, #29, #2072 ),
 .UNSPECIFIED., .F., .F.,
 ( 6, 3, 3, 6 ),
 ( 0.000000000000000000, 2.408321940520000037, 4.816680738749999691, 4.935551033660000364 ),
 .UNSPECIFIED. ) ;
#26751=LINE ( 'NONE', #7852, #7047 ) ;
#26764=CARTESIAN_POINT ( 'NONE',  ( 1.656896971990419853, -20.50178133589399110, -27.47978228995554417 ) ) ;
#26776=EDGE_LOOP ( 'NONE', ( #2857, #4801, #127, #5524 ) ) ;
#26786=ORIENTED_EDGE ( 'NONE', *, *, #3309, .T. ) ;
#26826=CARTESIAN_POINT ( 'NONE',  ( -3.982632971385688947, -19.71206033698065596, -27.86495495700036784 ) ) ;
#26831=VERTEX_POINT ( 'NONE', #2134 ) ;
#26856=B_SPLINE_CURVE_WITH_KNOTS ( 'NONE', 5,
 ( #7577, #23300, #25667, #20618, #20777, #27856, #22828, #27692, #4097, #13696, #15580, #6607, #25349, #15901, #1746 ),
 .UNSPECIFIED., .F., .F.,
 ( 6, 3, 3, 3, 6 ),
 ( 7.679355244459999952, 8.437083003899999767, 11.24945694400000029, 14.06183523920000056, 15.35825106630000114 ),
 .UNSPECIFIED. ) ;
#26925=CARTESIAN_POINT ( 'NONE',  ( 1.638687372170419598, -20.50181238077955470, -27.47976714835314738 ) ) ;
#26935=CARTESIAN_POINT ( 'NONE',  ( -1.861312627829580402, -20.50181238076562096, -27.47976714835994727 ) ) ;
#26973=EDGE_LOOP ( 'NONE', ( #6461, #30392, #18155, #2329 ) ) ;
#26980=ADVANCED_FACE ( 'NONE', ( #28637 ), #18137, .F. ) ;
#26994=FACE_OUTER_BOUND ( 'NONE', #24999, .T. ) ;
#27006=ORIENTED_EDGE ( 'NONE', *, *, #9107, .T. ) ;
#27051=ORIENTED_EDGE ( 'NONE', *, *, #20909, .F. ) ;
#27061=DIRECTION ( 'NONE',  ( 4.428977494234582379E-12, 0.8987940462991651502, -0.4383711467890810676 ) ) ;
#27089=LINE ( 'NONE', #5525, #11179 ) ;
#27117=CARTESIAN_POINT ( 'NONE',  ( 4.639038166103790495, -9.671115015700310735, -32.76225121019675157 ) ) ;
#27125=ORIENTED_EDGE ( 'NONE', *, *, #5870, .T. ) ;
#27132=ADVANCED_FACE ( 'NONE', ( #12414 ), #5172, .T. ) ;
#27141=CARTESIAN_POINT ( 'NONE',  ( -4.861312627816292142, -17.80543024185618606, -28.79488058873301171 ) ) ;
#27166=CARTESIAN_POINT ( 'NONE',  ( 1.645540681903832070, 2.658966097310066168, -42.11383941009797383 ) ) ;
#27223=CARTESIAN_POINT ( 'NONE',  ( -7.861312627756137594, -6.912605513598457208, -37.44547201166600559 ) ) ;
#27229=CARTESIAN_POINT ( 'NONE',  ( -7.300482373339721498, -8.173122728246529078, -36.83067668763386848 ) ) ;
#27276=EDGE_LOOP ( 'NONE', ( #20339, #26786, #2371, #9875 ) ) ;
#27289=ADVANCED_FACE ( 'NONE', ( #29559 ), #13029, .T. ) ;
#27314=LINE ( 'NONE', #20228, #14275 ) ;
#27405=EDGE_CURVE ( 'NONE', #10264, #13631, #24669, .T. ) ;
#27412=CARTESIAN_POINT ( 'NONE',  ( 5.423538825346226666, 5.076873815721838490, -43.29313180051233445 ) ) ;
#27419=VERTEX_POINT ( 'NONE', #614 ) ;
#27434=B_SPLINE_CURVE_WITH_KNOTS ( 'NONE', 3,
 ( #17951, #8356, #27412, #29621, #5393, #27561 ),
 .UNSPECIFIED., .F., .F.,
 ( 4, 2, 4 ),
 ( 0.000000000000000000, 0.5000000000000000000, 1.000000000000000000 ),
 .UNSPECIFIED. ) ;
#27464=CARTESIAN_POINT ( 'NONE',  ( 2.760998891309374148, 1.965471783823139473, -41.77559963342530125 ) ) ;
#27503=ORIENTED_EDGE ( 'NONE', *, *, #18161, .T. ) ;
#27530=CARTESIAN_POINT ( 'NONE',  ( -7.428071722523742260, -8.043573579563092935, -36.89386202926774416 ) ) ;
#27551=CARTESIAN_POINT ( 'NONE',  ( -7.861312627696711353, 6.462009008233210672, -40.63090155204401555 ) ) ;
#27561=CARTESIAN_POINT ( 'NONE',  ( 6.760007715859396527, 4.357143524031256376, -42.94209588227683128 ) ) ;
#27564=LINE ( 'NONE', #10163, #5734 ) ;
#27638=EDGE_CURVE ( 'NONE', #5034, #3507, #9542, .T. ) ;
#27657=DIRECTION ( 'NONE',  ( 5.962915006522623408E-16, 0.4383711467890811231, 0.8987940462991652613 ) ) ;
#27659=ORIENTED_EDGE ( 'NONE', *, *, #24428, .F. ) ;
#27691=DIRECTION ( 'NONE',  ( -5.962915006522622422E-16, -0.4383711467890810676, -0.8987940462991651502 ) ) ;
#27692=CARTESIAN_POINT ( 'NONE',  ( 3.763816007347946968, -0.7100252077446855825, -37.13286673860216069 ) ) ;
#27705=CARTESIAN_POINT ( 'NONE',  ( -5.415640807596865614, 6.430466356693489871, -40.61551717295832731 ) ) ;
#27726=CARTESIAN_POINT ( 'NONE',  ( 3.938868613454878709, -1.397147637169312340, -40.13554055886279315 ) ) ;
#27855=LINE ( 'NONE', #8809, #23400 ) ;
#27856=CARTESIAN_POINT ( 'NONE',  ( 4.006286404973145032, 0.3445522835526793060, -37.64721854827592296 ) ) ;
#27886=CARTESIAN_POINT ( 'NONE',  ( -1.861312627829582400, -21.81692582113286960, -30.17614928725744150 ) ) ;
#27935=VERTEX_POINT ( 'NONE', #10773 ) ;
#27940=DIRECTION ( 'NONE',  ( -1.000000000000000000, 3.981000000000000101E-12, -1.940999999999999908E-12 ) ) ;
#27970=CARTESIAN_POINT ( 'NONE',  ( 7.635581859131290727, 4.027124264807724785, -39.44332891327358226 ) ) ;
#27974=ORIENTED_EDGE ( 'NONE', *, *, #23844, .T. ) ;
#28023=CARTESIAN_POINT ( 'NONE',  ( -6.835848593969952702, 5.804179925720610811, -40.31005687079623812 ) ) ;
#28029=AXIS2_PLACEMENT_3D ( 'NONE', #8500, #28329, #4106 ) ;
#28113=DIRECTION ( 'NONE',  ( 1.000000000000000000, -3.981005269678786617E-12, 1.941197879946729322E-12 ) ) ;
#28136=ORIENTED_EDGE ( 'NONE', *, *, #13851, .T. ) ;
#28155=CARTESIAN_POINT ( 'NONE',  ( 5.647879864692651353, 6.332564579978557262, -40.56776728597595394 ) ) ;
#28216=EDGE_CURVE ( 'NONE', #6144, #22030, #3335, .T. ) ;
#28234=DIRECTION ( 'NONE',  ( 0.8366600265317032381, -0.4922897737126532003, 0.2401057656573751253 ) ) ;
#28236=ORIENTED_EDGE ( 'NONE', *, *, #24709, .F. ) ;
#28276=EDGE_CURVE ( 'NONE', #5864, #19664, #30716, .T. ) ;
#28293=VECTOR ( 'NONE', #24910, 1000.000000000000114 ) ;
#28311=CARTESIAN_POINT ( 'NONE',  ( -1.861312627829580402, -20.50181238076562096, -27.47976714835994727 ) ) ;
#28329=DIRECTION ( 'NONE',  ( 5.962915006522623408E-16, 0.4383711467890810676, 0.8987940462991651502 ) ) ;
#28350=CARTESIAN_POINT ( 'NONE',  ( -2.255103148512942468, -21.81692582113129575, -30.17614928725820533 ) ) ;
#28367=VECTOR ( 'NONE', #8683, 1000.000000000000114 ) ;
#28374=B_SPLINE_CURVE_WITH_KNOTS ( 'NONE', 5,
 ( #25467, #9082, #3901, #20736, #18677, #8766, #18375, #27970, #16780, #28439, #16936, #19307 ),
 .UNSPECIFIED., .F., .F.,
 ( 6, 3, 3, 6 ),
 ( 3.339306056889999930, 4.810258468999999870, 6.613963840320000287, 6.678484285959999767 ),
 .UNSPECIFIED. ) ;
#28439=CARTESIAN_POINT ( 'NONE',  ( 7.638652831670083465, 3.781993549609147465, -39.32377067501277423 ) ) ;
#28543=ORIENTED_EDGE ( 'NONE', *, *, #26577, .T. ) ;
#28553=DIRECTION ( 'NONE',  ( 5.962915006522623408E-16, 0.4383711467890811231, 0.8987940462991652613 ) ) ;
#28579=UNCERTAINTY_MEASURE_WITH_UNIT (LENGTH_MEASURE( 1.000000000000000082E-05 ), #2447, 'distance_accuracy_value', 'NONE');
#28609=FACE_OUTER_BOUND ( 'NONE', #16519, .T. ) ;
#28637=FACE_OUTER_BOUND ( 'NONE', #26776, .T. ) ;
#28665=CARTESIAN_POINT ( 'NONE',  ( 7.638687372243864182, -5.597492073922072819, -34.74908987243156133 ) ) ;
#28715=ADVANCED_FACE ( 'NONE', ( #30459 ), #16585, .T. ) ;
#28743=ORIENTED_EDGE ( 'NONE', *, *, #4787, .F. ) ;
#28762=ORIENTED_EDGE ( 'NONE', *, *, #8467, .T. ) ;
#28767=DIRECTION ( 'NONE',  ( 5.962915006522623408E-16, 0.4383711467890810676, 0.8987940462991651502 ) ) ;
#28780=DIRECTION ( 'NONE',  ( 5.962915006522623408E-16, 0.4383711467890811231, 0.8987940462991652613 ) ) ;
#28800=DIRECTION ( 'NONE',  ( 1.000000000000000000, -3.981000000000000101E-12, 1.940999999999999908E-12 ) ) ;
#28864=( NAMED_UNIT ( * ) SI_UNIT ( $, .STERADIAN. ) SOLID_ANGLE_UNIT ( ) );
#28905=CARTESIAN_POINT ( 'NONE',  ( 7.259803861751887410, 3.808917229486211031, -42.67470805251851829 ) ) ;
#28917=CYLINDRICAL_SURFACE ( 'NONE', #23235, 4.099999999999997868 ) ;
#28935=CARTESIAN_POINT ( 'NONE',  ( 4.259937771191533606, -20.47891468366403345, -30.82874092286507306 ) ) ;
#28944=DIRECTION ( 'NONE',  ( 5.962915006522623408E-16, 0.4383711467890811231, 0.8987940462991652613 ) ) ;
#28970=CARTESIAN_POINT ( 'NONE',  ( 2.193015549840575229, -20.47026972997080563, -27.49515152708232790 ) ) ;
#29007=DIRECTION ( 'NONE',  ( 5.962915006522622422E-16, 0.4383711467890810676, 0.8987940462991651502 ) ) ;
#29051=EDGE_CURVE ( 'NONE', #8590, #9948, #6779, .T. ) ;
#29057=CARTESIAN_POINT ( 'NONE',  ( 6.760007715859396527, 4.357143524031256376, -42.94209588227683128 ) ) ;
#29103=EDGE_CURVE ( 'NONE', #24186, #30146, #5365, .T. ) ;
#29114=DIRECTION ( 'NONE',  ( 5.962915006522623408E-16, 0.4383711467890811231, 0.8987940462991652613 ) ) ;
#29153=CARTESIAN_POINT ( 'NONE',  ( 7.638687372303289536, 6.462009008171509805, -40.63090155201393117 ) ) ;
#29180=B_SPLINE_CURVE_WITH_KNOTS ( 'NONE', 3,
 ( #24432, #207, #24269, #370 ),
 .UNSPECIFIED., .F., .F.,
 ( 4, 4 ),
 ( 0.000000000000000000, 1.000000000000000000 ),
 .UNSPECIFIED. ) ;
#29189=CARTESIAN_POINT ( 'NONE',  ( 2.033218777617324502, -21.81692582114836654, -30.17614928724987777 ) ) ;
#29203=DIRECTION ( 'NONE',  ( 1.000000000000000000, 0.000000000000000000, 0.000000000000000000 ) ) ;
#29210=ORIENTED_EDGE ( 'NONE', *, *, #22290, .T. ) ;
#29227=CARTESIAN_POINT ( 'NONE',  ( -4.861312627796362307, -13.76085703350993228, -30.76755074928387401 ) ) ;
#29240=VECTOR ( 'NONE', #3264, 1000.000000000000114 ) ;
#29281=CARTESIAN_POINT ( 'NONE',  ( -2.540108707139367539, -20.45867351756849928, -27.50080737777486561 ) ) ;
#29295=ORIENTED_EDGE ( 'NONE', *, *, #157, .F. ) ;
#29312=EDGE_LOOP ( 'NONE', ( #15643, #28236, #13217, #266 ) ) ;
#29335=CARTESIAN_POINT ( 'NONE',  ( -4.768428784999852788, -18.52815030097902493, -28.44238646348855681 ) ) ;
#29349=VECTOR ( 'NONE', #12700, 1000.000000000000114 ) ;
#29394=FACE_OUTER_BOUND ( 'NONE', #22216, .T. ) ;
#29425=PRODUCT_DEFINITION_FORMATION_WITH_SPECIFIED_SOURCE ( 'ANY', '', #29916, .NOT_KNOWN. ) ;
#29456=ADVANCED_FACE ( 'NONE', ( #29394 ), #16658, .F. ) ;
#29477=CARTESIAN_POINT ( 'NONE',  ( -4.084346732781014566, 1.529807325146986807, -38.22530605782345958 ) ) ;
#29499=VERTEX_POINT ( 'NONE', #2361 ) ;
#29559=FACE_OUTER_BOUND ( 'NONE', #11468, .T. ) ;
#29584=CARTESIAN_POINT ( 'NONE',  ( -7.534632680830990026, -7.897185061638417380, -36.96526048005145526 ) ) ;
#29605=VECTOR ( 'NONE', #2602, 1000.000000000000114 ) ;
#29621=CARTESIAN_POINT ( 'NONE',  ( 6.150013584267105315, 4.806477681428259707, -43.16125079399513709 ) ) ;
#29623=CARTESIAN_POINT ( 'NONE',  ( -7.861312627756137594, -6.255048793414832886, -36.09728094221726025 ) ) ;
#29631=ORIENTED_EDGE ( 'NONE', *, *, #28276, .F. ) ;
#29679=CARTESIAN_POINT ( 'NONE',  ( 3.750246723960807049, 0.6078790020706823505, -41.11345739176283587 ) ) ;
#29709=CARTESIAN_POINT ( 'NONE',  ( 6.438687372225744276, -8.560122214837054599, -36.64192442626541890 ) ) ;
#29728=DIRECTION ( 'NONE',  ( 5.962915006522622422E-16, 0.4383711467890810676, 0.8987940462991651502 ) ) ;
#29783=CARTESIAN_POINT ( 'NONE',  ( -0.9048562442035532616, 4.261764438836468827, -39.55777057273417086 ) ) ;
#29799=ORIENTED_EDGE ( 'NONE', *, *, #5870, .F. ) ;
#29824=CARTESIAN_POINT ( 'NONE',  ( -0.1113126277073495929, 2.989789856717120387, -42.27519293863267791 ) ) ;
#29859=AXIS2_PLACEMENT_3D ( 'NONE', #11536, #17968, #15622 ) ;
#29916=PRODUCT ( 'Drive Pawl', 'Drive Pawl', '', ( #5950 ) ) ;
#29948=DIRECTION ( 'NONE',  ( 5.962915006522623408E-16, 0.4383711467890811231, 0.8987940462991652613 ) ) ;
#29980=CARTESIAN_POINT ( 'NONE',  ( 0.3401257266749637687, 2.989789856715318717, -42.27519293863180394 ) ) ;
#30023=VECTOR ( 'NONE', #21533, 1000.000000000000114 ) ;
#30078=CARTESIAN_POINT ( 'NONE',  ( -6.676371816449358398, 5.924696735301250961, -40.36883684629870572 ) ) ;
#30098=FACE_OUTER_BOUND ( 'NONE', #23470, .T. ) ;
#30146=VERTEX_POINT ( 'NONE', #6961 ) ;
#30171=PRODUCT_DEFINITION_SHAPE ( 'NONE', 'NONE',  #7911 ) ;
#30220=ORIENTED_EDGE ( 'NONE', *, *, #20477, .T. ) ;
#30254=CARTESIAN_POINT ( 'NONE',  ( -7.534632680830988249, -6.582071621095836100, -34.26887834079445128 ) ) ;
#30274=DIRECTION ( 'NONE',  ( -5.962915006522622422E-16, -0.4383711467890810676, -0.8987940462991651502 ) ) ;
#30282=CARTESIAN_POINT ( 'NONE',  ( -4.861312627776431583, -9.716283825163692711, -32.74022090983473987 ) ) ;
#30291=CARTESIAN_POINT ( 'NONE',  ( -3.982632971385688947, -19.71206033698065596, -27.86495495700036784 ) ) ;
#30314=ADVANCED_FACE ( 'NONE', ( #14516 ), #9941, .T. ) ;
#30392=ORIENTED_EDGE ( 'NONE', *, *, #18259, .F. ) ;
#30393=B_SPLINE_CURVE_WITH_KNOTS ( 'NONE', 5,
 ( #12329, #21936, #14856, #9971, #24285, #12473, #3033, #10127, #9815 ),
 .UNSPECIFIED., .F., .F.,
 ( 6, 3, 6 ),
 ( 0.000000000000000000, 2.405120303199999920, 3.339306056609999906 ),
 .UNSPECIFIED. ) ;
#30395=VECTOR ( 'NONE', #17473, 1000.000000000000114 ) ;
#30399=LINE ( 'NONE', #26598, #1714 ) ;
#30403=CARTESIAN_POINT ( 'NONE',  ( -4.879522228196710110, 6.461977963245837842, -40.63088641039196602 ) ) ;
#30442=LINE ( 'NONE', #18467, #8618 ) ;
#30451=ORIENTED_EDGE ( 'NONE', *, *, #29103, .F. ) ;
#30459=FACE_OUTER_BOUND ( 'NONE', #4681, .T. ) ;
#30460=CARTESIAN_POINT ( 'NONE',  ( -4.084346732781014566, 1.529807325146986807, -38.22530605782345958 ) ) ;
#30503=ORIENTED_EDGE ( 'NONE', *, *, #20477, .F. ) ;
#30558=EDGE_CURVE ( 'NONE', #22416, #18028, #9979, .T. ) ;
#30583=DIRECTION ( 'NONE',  ( 0.7071067811834158556, -0.6355433650310500227, 0.3099752105724556395 ) ) ;
#30594=ADVANCED_FACE ( 'NONE', ( #3985 ), #18132, .T. ) ;
#30616=CARTESIAN_POINT ( 'NONE',  ( 5.638687372243864182, -5.597492073914120070, -34.74908987243544090 ) ) ;
#30628=ORIENTED_EDGE ( 'NONE', *, *, #18161, .F. ) ;
#30640=CARTESIAN_POINT ( 'NONE',  ( -7.861312627708255896, 2.804450004377710304, -42.18479665268674950 ) ) ;
#30657=DIRECTION ( 'NONE',  ( 1.000000000000000000, -3.981005269678786617E-12, 1.941197879946729322E-12 ) ) ;
#30659=SHAPE_REPRESENTATION ( 'Drive Pawl', ( #17722 ), #14795 ) ;
#30669=FACE_OUTER_BOUND ( 'NONE', #11061, .T. ) ;
#30687=ADVANCED_FACE ( 'NONE', ( #1941 ), #1478, .T. ) ;
#30716=LINE ( 'NONE', #3970, #21344 ) ;
#30717=CARTESIAN_POINT ( 'NONE',  ( 4.638687372303289536, 6.462009008183451364, -40.63090155201975762 ) ) ;
#30803=CARTESIAN_POINT ( 'NONE',  ( -7.534632680830988249, -6.582071621271182060, -34.26887834115397169 ) ) ;
#30818=ADVANCED_FACE ( 'NONE', ( #14057 ), #23661, .F. ) ;
#30850=ORIENTED_EDGE ( 'NONE', *, *, #15014, .F. ) ;
#30882=STYLED_ITEM ( 'NONE', ( #24302 ), #12524 ) ;
#30922=ADVANCED_FACE ( 'NONE', ( #364 ), #3012, .T. ) ;
#30932=ORIENTED_EDGE ( 'NONE', *, *, #20661, .F. ) ;
#30993=EDGE_CURVE ( 'NONE', #22535, #528, #26856, .T. ) ;
#31003=ORIENTED_EDGE ( 'NONE', *, *, #26704, .T. ) ;
#31030=CARTESIAN_POINT ( 'NONE',  ( 7.312007425309012376, -6.582071621330287670, -34.26887834112514497 ) ) ;
#31118=CLOSED_SHELL ( 'NONE', ( #1187, #26980, #30594, #5448, #13109, #30687, #27289, #21987, #29456, #27132, #30922, #2485, #30314, #14467, #13671, #17206, #11000, #18625, #28715, #12903, #23373, #23705, #558, #21059, #17554, #9826, #12664, #30818 ) ) ;
ENDSEC;
END-ISO-10303-21;
